ISO-10303-21;
HEADER;
/* Generated by software containing ST-Developer
 * from STEP Tools, Inc. (www.steptools.com) 
 */
/* OPTION: using custom renumber hook */

FILE_DESCRIPTION(
/* description */ ('STEP AP242 Edition 2', 'CAx-IF Rec.Pracs.---Representation and Presentation of Product Manufa
cturing Information (PMI)---4.0---2014-10-13', 'CAx-IF Rec.Pracs.---3D Tessellated Geometry---0.4---2014-09-14', '2;1', 'CAx-IF Rec.Pracs.---User Defined Attributes---1.5---2016-08-15'),
/* implementation_level */ '2;1');

FILE_NAME(
/* name */ 'refill_cap__PD45595.step',
/* time_stamp */ '2026-10-08T12:15:07Z',
/* author */ (''),
/* organization */ (''),
/* preprocessor_version */ 'ST-DEVELOPER v20',
/* originating_system */ 'ONSHAPE BY PTC INC, 1.221',
/* authorisation */ '  ');

FILE_SCHEMA (('AP242_MANAGED_MODEL_BASED_3D_ENGINEERING_MIM_LF { 1 0 10303 442 3 1 4 }'));
ENDSEC;

DATA;
#54=B_SPLINE_SURFACE_WITH_KNOTS('',3,3,((#33420,#33421,#33422,#33423,#33424,
#33425),(#33426,#33427,#33428,#33429,#33430,#33431),(#33432,#33433,#33434,
#33435,#33436,#33437),(#33438,#33439,#33440,#33441,#33442,#33443)),
 .UNSPECIFIED.,.F.,.F.,.F.,(4,4),(4,2,4),(-0.00600752213313948,1.),(0.796322545918902,
0.814827939626118,0.833333333333333),.UNSPECIFIED.);
#60=COLOUR_RGB('', 0.66274510, 0.83137255, 0.94901961);
#210=SHAPE_REPRESENTATION_RELATIONSHIP('','',#13784,#237);
#237=ADVANCED_BREP_SHAPE_REPRESENTATION('',(#13728),#45474);
#602=CIRCLE('',#14300,0.000762);
#603=CIRCLE('',#14301,0.000762000000000046);
#604=CIRCLE('',#14302,0.000762000000000038);
#605=CIRCLE('',#14304,0.0081692);
#606=CIRCLE('',#14306,0.000254);
#607=CIRCLE('',#14307,0.000254000000000014);
#608=CIRCLE('',#14309,0.009236);
#609=CIRCLE('',#14310,0.009236);
#610=CIRCLE('',#14313,0.000253999999999972);
#611=CIRCLE('',#14314,0.00840975562057229);
#612=CIRCLE('',#14316,0.009236);
#613=CIRCLE('',#14318,0.009236);
#614=CIRCLE('',#14319,0.012);
#615=CIRCLE('',#14321,0.012);
#616=CIRCLE('',#14323,0.009236);
#617=CIRCLE('',#14324,0.01);
#618=CIRCLE('',#14326,0.008);
#619=CIRCLE('',#14328,0.01);
#620=CIRCLE('',#14329,0.008);
#1100=B_SPLINE_CURVE_WITH_KNOTS('',3,(#32285,#32286,#32287,#32288),
 .UNSPECIFIED.,.F.,.F.,(4,4),(0.,0.00676281690826917),.UNSPECIFIED.);
#1101=B_SPLINE_CURVE_WITH_KNOTS('',3,(#32585,#32586,#32587,#32588,#32589),
 .UNSPECIFIED.,.F.,.F.,(4,1,4),(0.,0.00441087142557483,0.00882174285114967),
 .UNSPECIFIED.);
#1102=B_SPLINE_CURVE_WITH_KNOTS('',3,(#32936,#32937,#32938,#32939,#32940,
#32941,#32942,#32943),.UNSPECIFIED.,.F.,.F.,(4,1,1,1,1,4),(5.05159101305033E-17,
0.000510091042055662,0.00102018208411127,0.0020403641682225,0.00306054625233372,
0.00408072833644494),.UNSPECIFIED.);
#1103=B_SPLINE_CURVE_WITH_KNOTS('',3,(#33096,#33097,#33098,#33099),
 .UNSPECIFIED.,.F.,.F.,(4,4),(6.05912861432085E-17,0.00208718873665751),
 .UNSPECIFIED.);
#1104=B_SPLINE_CURVE_WITH_KNOTS('',3,(#33296,#33297,#33298,#33299,#33300,
#33301,#33302,#33303),.UNSPECIFIED.,.F.,.F.,(4,1,1,1,1,4),(0.,0.00114202028985642,
0.00228404057971283,0.00342606086956925,0.00399707101449746,0.00456808115942567),
 .UNSPECIFIED.);
#1105=B_SPLINE_CURVE_WITH_KNOTS('',3,(#33362,#33363,#33364,#33365),
 .UNSPECIFIED.,.F.,.F.,(4,4),(0.,0.000338478963180613),.UNSPECIFIED.);
#1106=B_SPLINE_CURVE_WITH_KNOTS('',3,(#33404,#33405,#33406,#33407,#33408,
#33409,#33410,#33411),.UNSPECIFIED.,.F.,.F.,(4,1,1,1,1,4),(0.,0.000572817003192511,
0.00114563400638502,0.00229126801277004,0.00343690201915507,0.00458253602554009),
 .UNSPECIFIED.);
#1107=B_SPLINE_CURVE_WITH_KNOTS('',3,(#33446,#33447,#33448,#33449),
 .UNSPECIFIED.,.F.,.F.,(4,4),(8.39720847001417E-16,0.00208289890788513),
 .UNSPECIFIED.);
#1108=B_SPLINE_CURVE_WITH_KNOTS('',3,(#33462,#33463,#33464,#33465,#33466,
#33467,#33468,#33469),.UNSPECIFIED.,.F.,.F.,(4,1,1,1,1,4),(4.60907911065496E-11,
0.000959696893981847,0.0019193937418729,0.00287909058976396,0.00335893901370949,
0.00383878743765501),.UNSPECIFIED.);
#1278=PLANE('',#14305);
#1279=PLANE('',#14311);
#1280=PLANE('',#14312);
#1281=PLANE('',#14317);
#1282=PLANE('',#14320);
#1283=PLANE('',#14322);
#1284=PLANE('',#14325);
#1285=PLANE('',#14327);
#1624=CYLINDRICAL_SURFACE('',#14303,0.0081692);
#1625=CYLINDRICAL_SURFACE('',#14308,0.009236);
#1626=CYLINDRICAL_SURFACE('',#14315,0.009236);
#1627=CYLINDRICAL_SURFACE('',#14330,0.01);
#1628=CYLINDRICAL_SURFACE('',#14331,0.008);
#1629=CYLINDRICAL_SURFACE('',#14332,0.009236);
#1630=CYLINDRICAL_SURFACE('',#14333,0.012);
#1876=(
BOUNDED_CURVE()
B_SPLINE_CURVE(2,(#31969,#31970,#31971,#31972,#31973,#31974,#31975,#31976,
#31977,#31978,#31979,#31980,#31981,#31982,#31983,#31984,#31985,#31986,#31987,
#31988,#31989,#31990,#31991,#31992,#31993,#31994,#31995,#31996,#31997,#31998,
#31999,#32000,#32001,#32002,#32003,#32004,#32005,#32006,#32007,#32008,#32009,
#32010,#32011,#32012,#32013,#32014,#32015,#32016,#32017,#32018,#32019,#32020,
#32021,#32022,#32023,#32024,#32025,#32026,#32027,#32028,#32029),
 .UNSPECIFIED.,.F.,.F.)
B_SPLINE_CURVE_WITH_KNOTS((3,2,2,2,2,2,2,2,2,2,2,2,2,2,2,2,2,2,2,2,2,2,
2,2,2,2,2,2,2,2,3),(0.,0.0277777777777778,0.0555555555555556,0.0833333333333333,
0.111111111111111,0.138888888888889,0.166666666666667,0.194444444444445,
0.222222222222222,0.25,0.277777777777778,0.305555555555555,0.333333333333334,
0.361111111111111,0.388888888888889,0.416666666666667,0.444444444444444,
0.472222222222222,0.5,0.527777777777778,0.555555555555556,0.583333333333333,
0.611111111111111,0.638888888888889,0.666666666666667,0.694444444444444,
0.722222222222222,0.75,0.777777777777778,0.805555555555556,0.833333333333333),
 .UNSPECIFIED.)
CURVE()
GEOMETRIC_REPRESENTATION_ITEM()
RATIONAL_B_SPLINE_CURVE((1.,0.965925826289068,1.,0.965925826289068,1.,0.965925826289068,
1.,0.965925826289068,1.,0.965925826289068,1.,0.965925826289068,1.,0.965925826289068,
1.,0.965925826289068,1.,0.965925826289068,1.,0.965925826289068,1.,0.965925826289068,
1.,0.965925826289068,1.,0.965925826289068,1.,0.965925826289068,1.,0.965925826289068,
1.,0.965925826289068,1.,0.965925826289068,1.,0.965925826289068,1.,0.965925826289068,
1.,0.965925826289068,1.,0.965925826289068,1.,0.965925826289068,1.,0.965925826289068,
1.,0.965925826289068,1.,0.965925826289068,1.,0.965925826289068,1.,0.965925826289068,
1.,0.965925826289068,1.,0.965925826289068,1.,0.965925826289068,1.))
REPRESENTATION_ITEM('')
);
#1877=(
BOUNDED_CURVE()
B_SPLINE_CURVE(2,(#32033,#32034,#32035,#32036,#32037,#32038,#32039,#32040,
#32041,#32042,#32043,#32044,#32045),.UNSPECIFIED.,.F.,.F.)
B_SPLINE_CURVE_WITH_KNOTS((3,2,2,2,2,2,3),(0.666666666666666,0.694444444444444,
0.722222222222222,0.75,0.777777777777778,0.805555555555556,0.833333333333333),
 .UNSPECIFIED.)
CURVE()
GEOMETRIC_REPRESENTATION_ITEM()
RATIONAL_B_SPLINE_CURVE((1.,0.965925826289068,1.,0.965925826289068,1.,0.965925826289068,
1.,0.965925826289068,1.,0.965925826289068,1.,0.965925826289068,1.))
REPRESENTATION_ITEM('')
);
#1878=(
BOUNDED_CURVE()
B_SPLINE_CURVE(2,(#32047,#32048,#32049,#32050,#32051,#32052,#32053,#32054,
#32055,#32056,#32057,#32058,#32059),.UNSPECIFIED.,.F.,.F.)
B_SPLINE_CURVE_WITH_KNOTS((3,2,2,2,2,2,3),(0.5,0.527777777777778,0.555555555555556,
0.583333333333333,0.611111111111111,0.638888888888889,0.666666666666666),
 .UNSPECIFIED.)
CURVE()
GEOMETRIC_REPRESENTATION_ITEM()
RATIONAL_B_SPLINE_CURVE((1.,0.965925826289069,1.,0.965925826289068,1.,0.965925826289068,
1.,0.965925826289068,1.,0.965925826289068,1.,0.965925826289069,1.))
REPRESENTATION_ITEM('')
);
#1879=(
BOUNDED_CURVE()
B_SPLINE_CURVE(2,(#32061,#32062,#32063,#32064,#32065,#32066,#32067,#32068,
#32069,#32070,#32071,#32072,#32073),.UNSPECIFIED.,.F.,.F.)
B_SPLINE_CURVE_WITH_KNOTS((3,2,2,2,2,2,3),(0.333333333333333,0.361111111111111,
0.388888888888889,0.416666666666667,0.444444444444444,0.472222222222222,
0.5),.UNSPECIFIED.)
CURVE()
GEOMETRIC_REPRESENTATION_ITEM()
RATIONAL_B_SPLINE_CURVE((1.,0.965925826289068,1.,0.965925826289068,1.,0.965925826289068,
1.,0.965925826289068,1.,0.965925826289068,1.,0.965925826289068,1.))
REPRESENTATION_ITEM('')
);
#1880=(
BOUNDED_CURVE()
B_SPLINE_CURVE(2,(#32075,#32076,#32077,#32078,#32079,#32080,#32081,#32082,
#32083,#32084,#32085,#32086,#32087),.UNSPECIFIED.,.F.,.F.)
B_SPLINE_CURVE_WITH_KNOTS((3,2,2,2,2,2,3),(0.166666666666668,0.194444444444445,
0.222222222222222,0.25,0.277777777777778,0.305555555555555,0.333333333333333),
 .UNSPECIFIED.)
CURVE()
GEOMETRIC_REPRESENTATION_ITEM()
RATIONAL_B_SPLINE_CURVE((1.,0.965925826289069,1.,0.965925826289068,1.,0.965925826289068,
1.,0.965925826289068,1.,0.965925826289068,1.,0.965925826289069,1.))
REPRESENTATION_ITEM('')
);
#1881=(
BOUNDED_CURVE()
B_SPLINE_CURVE(2,(#32089,#32090,#32091,#32092,#32093,#32094,#32095,#32096,
#32097,#32098,#32099,#32100,#32101),.UNSPECIFIED.,.F.,.F.)
B_SPLINE_CURVE_WITH_KNOTS((3,2,2,2,2,2,3),(0.,0.0277777777777779,0.0555555555555558,
0.0833333333333336,0.111111111111111,0.138888888888889,0.166666666666668),
 .UNSPECIFIED.)
CURVE()
GEOMETRIC_REPRESENTATION_ITEM()
RATIONAL_B_SPLINE_CURVE((1.,0.965925826289068,1.,0.965925826289068,1.,0.965925826289068,
1.,0.965925826289068,1.,0.965925826289068,1.,0.965925826289068,1.))
REPRESENTATION_ITEM('')
);
#1882=(
BOUNDED_CURVE()
B_SPLINE_CURVE(2,(#32224,#32225,#32226,#32227,#32228,#32229,#32230,#32231,
#32232,#32233,#32234,#32235,#32236,#32237,#32238,#32239,#32240,#32241,#32242,
#32243,#32244,#32245,#32246,#32247,#32248,#32249,#32250,#32251,#32252,#32253,
#32254,#32255,#32256,#32257,#32258,#32259,#32260,#32261,#32262,#32263,#32264,
#32265,#32266,#32267,#32268,#32269,#32270,#32271,#32272,#32273,#32274,#32275,
#32276,#32277,#32278,#32279,#32280,#32281,#32282),.UNSPECIFIED.,.F.,.F.)
B_SPLINE_CURVE_WITH_KNOTS((3,2,2,2,2,2,2,2,2,2,2,2,2,2,2,2,2,2,2,2,2,2,
2,2,2,2,2,2,2,3),(0.,0.0277777777777778,0.0555555555555556,0.0833333333333333,
0.111111111111111,0.138888888888889,0.166666666666667,0.194444444444445,
0.222222222222222,0.25,0.277777777777778,0.305555555555555,0.333333333333334,
0.361111111111111,0.388888888888889,0.416666666666667,0.444444444444444,
0.472222222222222,0.5,0.527777777777778,0.555555555555556,0.583333333333333,
0.611111111111111,0.638888888888889,0.666666666666667,0.694444444444444,
0.722222222222222,0.75,0.777777777777778,0.791679968730667),
 .UNSPECIFIED.)
CURVE()
GEOMETRIC_REPRESENTATION_ITEM()
RATIONAL_B_SPLINE_CURVE((1.,0.965925826289068,1.,0.965925826289068,1.,0.965925826289068,
1.,0.965925826289068,1.,0.965925826289068,1.,0.965925826289068,1.,0.965925826289068,
1.,0.965925826289068,1.,0.965925826289068,1.,0.965925826289068,1.,0.965925826289068,
1.,0.965925826289068,1.,0.965925826289068,1.,0.965925826289068,1.,0.965925826289068,
1.,0.965925826289068,1.,0.965925826289068,1.,0.965925826289068,1.,0.965925826289068,
1.,0.965925826289068,1.,0.965925826289068,1.,0.965925826289068,1.,0.965925826289068,
1.,0.965925826289068,1.,0.965925826289068,1.,0.965925826289068,1.,0.965925826289068,
1.,0.965925826289068,1.,0.982946595898313,0.982962928772354))
REPRESENTATION_ITEM('')
);
#1883=(
BOUNDED_CURVE()
B_SPLINE_CURVE(2,(#32528,#32529,#32530,#32531,#32532,#32533,#32534,#32535,
#32536,#32537,#32538,#32539,#32540,#32541,#32542,#32543,#32544,#32545,#32546,
#32547,#32548,#32549,#32550,#32551,#32552,#32553,#32554,#32555,#32556,#32557,
#32558,#32559,#32560,#32561,#32562,#32563,#32564,#32565,#32566,#32567,#32568,
#32569,#32570,#32571,#32572,#32573,#32574,#32575,#32576,#32577,#32578,#32579,
#32580,#32581,#32582),.UNSPECIFIED.,.F.,.F.)
B_SPLINE_CURVE_WITH_KNOTS((3,2,2,2,2,2,2,2,2,2,2,2,2,2,2,2,2,2,2,2,2,2,
2,2,2,2,2,3),(0.,0.0277777777777778,0.0555555555555556,0.0833333333333333,
0.111111111111111,0.138888888888889,0.166666666666667,0.194444444444445,
0.222222222222222,0.25,0.277777777777778,0.305555555555555,0.333333333333334,
0.361111111111111,0.388888888888889,0.416666666666667,0.444444444444444,
0.472222222222222,0.5,0.527777777777778,0.555555555555556,0.583333333333333,
0.611111111111111,0.638888888888889,0.666666666666667,0.694444444444444,
0.722222222222222,0.735128599370391),.UNSPECIFIED.)
CURVE()
GEOMETRIC_REPRESENTATION_ITEM()
RATIONAL_B_SPLINE_CURVE((1.,0.965925826289068,1.,0.965925826289068,1.,0.965925826289068,
1.,0.965925826289068,1.,0.965925826289068,1.,0.965925826289068,1.,0.965925826289068,
1.,0.965925826289068,1.,0.965925826289068,1.,0.965925826289068,1.,0.965925826289068,
1.,0.965925826289068,1.,0.965925826289068,1.,0.965925826289068,1.,0.965925826289068,
1.,0.965925826289068,1.,0.965925826289068,1.,0.965925826289068,1.,0.965925826289068,
1.,0.965925826289068,1.,0.965925826289068,1.,0.965925826289068,1.,0.965925826289068,
1.,0.965925826289068,1.,0.965925826289068,1.,0.965925826289068,1.,0.984168131070682,
0.983048171279439))
REPRESENTATION_ITEM('')
);
#1884=(
BOUNDED_CURVE()
B_SPLINE_CURVE(2,(#32592,#32593,#32594,#32595,#32596,#32597,#32598,#32599,
#32600,#32601,#32602,#32603,#32604,#32605,#32606,#32607,#32608,#32609,#32610,
#32611,#32612,#32613,#32614,#32615,#32616,#32617,#32618,#32619,#32620,#32621,
#32622,#32623,#32624,#32625,#32626,#32627,#32628,#32629,#32630,#32631,#32632,
#32633,#32634,#32635,#32636,#32637,#32638,#32639,#32640,#32641,#32642,#32643,
#32644),.UNSPECIFIED.,.F.,.F.)
B_SPLINE_CURVE_WITH_KNOTS((3,2,2,2,2,2,2,2,2,2,2,2,2,2,2,2,2,2,2,2,2,2,
2,2,2,2,3),(0.,0.0277777777777778,0.0555555555555556,0.0833333333333333,
0.111111111111111,0.138888888888889,0.166666666666667,0.194444444444445,
0.222222222222222,0.25,0.277777777777778,0.305555555555555,0.333333333333334,
0.361111111111111,0.388888888888889,0.416666666666667,0.444444444444444,
0.472222222222222,0.5,0.527777777777778,0.555555555555556,0.583333333333333,
0.611111111111111,0.638888888888889,0.666666666666667,0.694444444444444,
0.698457242498421),.UNSPECIFIED.)
CURVE()
GEOMETRIC_REPRESENTATION_ITEM()
RATIONAL_B_SPLINE_CURVE((1.,0.965925826289068,1.,0.965925826289068,1.,0.965925826289068,
1.,0.965925826289068,1.,0.965925826289068,1.,0.965925826289068,1.,0.965925826289068,
1.,0.965925826289068,1.,0.965925826289068,1.,0.965925826289068,1.,0.965925826289068,
1.,0.965925826289068,1.,0.965925826289068,1.,0.965925826289068,1.,0.965925826289068,
1.,0.965925826289068,1.,0.965925826289068,1.,0.965925826289068,1.,0.965925826289068,
1.,0.965925826289068,1.,0.965925826289068,1.,0.965925826289068,1.,0.965925826289068,
1.,0.965925826289068,1.,0.965925826289068,1.,0.995077619993509,0.991577421204609))
REPRESENTATION_ITEM('')
);
#1885=(
BOUNDED_CURVE()
B_SPLINE_CURVE(2,(#32663,#32664,#32665,#32666,#32667,#32668,#32669),
 .UNSPECIFIED.,.F.,.F.)
B_SPLINE_CURVE_WITH_KNOTS((3,2,2,3),(0.560471898984009,0.583333333333333,
0.611111111111111,0.633782023464906),.UNSPECIFIED.)
CURVE()
GEOMETRIC_REPRESENTATION_ITEM()
RATIONAL_B_SPLINE_CURVE((0.990073274378595,0.971956558529202,1.,0.965925826289068,
1.,0.972190266193773,0.989774519102187))
REPRESENTATION_ITEM('')
);
#1886=(
BOUNDED_CURVE()
B_SPLINE_CURVE(2,(#32884,#32885,#32886,#32887,#32888,#32889,#32890,#32891,
#32892,#32893,#32894,#32895,#32896,#32897,#32898,#32899,#32900,#32901,#32902,
#32903,#32904,#32905,#32906,#32907,#32908,#32909,#32910,#32911,#32912,#32913,
#32914,#32915,#32916,#32917,#32918,#32919,#32920,#32921,#32922,#32923,#32924,
#32925,#32926,#32927,#32928,#32929,#32930,#32931,#32932,#32933,#32934),
 .UNSPECIFIED.,.F.,.F.)
B_SPLINE_CURVE_WITH_KNOTS((3,2,2,2,2,2,2,2,2,2,2,2,2,2,2,2,2,2,2,2,2,2,
2,2,2,3),(0.,0.0277777777777778,0.0555555555555556,0.0833333333333333,0.111111111111111,
0.138888888888889,0.166666666666667,0.194444444444445,0.222222222222222,
0.25,0.277777777777778,0.305555555555555,0.333333333333334,0.361111111111111,
0.388888888888889,0.416666666666667,0.444444444444444,0.472222222222222,
0.5,0.527777777777778,0.555555555555556,0.583333333333333,0.611111111111111,
0.638888888888889,0.666666666666667,0.672203650950348),.UNSPECIFIED.)
CURVE()
GEOMETRIC_REPRESENTATION_ITEM()
RATIONAL_B_SPLINE_CURVE((1.,0.965925826289068,1.,0.965925826289068,1.,0.965925826289068,
1.,0.965925826289068,1.,0.965925826289068,1.,0.965925826289068,1.,0.965925826289068,
1.,0.965925826289068,1.,0.965925826289068,1.,0.965925826289068,1.,0.965925826289068,
1.,0.965925826289068,1.,0.965925826289068,1.,0.965925826289068,1.,0.965925826289068,
1.,0.965925826289068,1.,0.965925826289068,1.,0.965925826289068,1.,0.965925826289068,
1.,0.965925826289068,1.,0.965925826289068,1.,0.965925826289068,1.,0.965925826289068,
1.,0.965925826289068,1.,0.993207946084594,0.989123631865601))
REPRESENTATION_ITEM('')
);
#1887=(
BOUNDED_CURVE()
B_SPLINE_CURVE(2,(#33046,#33047,#33048,#33049,#33050,#33051,#33052,#33053,
#33054,#33055,#33056,#33057,#33058,#33059,#33060,#33061,#33062,#33063,#33064,
#33065,#33066,#33067,#33068,#33069,#33070,#33071,#33072,#33073,#33074,#33075,
#33076,#33077,#33078,#33079,#33080,#33081,#33082,#33083,#33084,#33085,#33086,
#33087,#33088,#33089,#33090,#33091,#33092,#33093,#33094),.UNSPECIFIED.,
 .F.,.F.)
B_SPLINE_CURVE_WITH_KNOTS((3,2,2,2,2,2,2,2,2,2,2,2,2,2,2,2,2,2,2,2,2,2,
2,2,3),(0.,0.0277777777777778,0.0555555555555556,0.0833333333333333,0.111111111111111,
0.138888888888889,0.166666666666667,0.194444444444445,0.222222222222222,
0.25,0.277777777777778,0.305555555555555,0.333333333333334,0.361111111111111,
0.388888888888889,0.416666666666667,0.444444444444444,0.472222222222222,
0.5,0.527777777777778,0.555555555555556,0.583333333333333,0.611111111111111,
0.638888888888889,0.660043255494719),.UNSPECIFIED.)
CURVE()
GEOMETRIC_REPRESENTATION_ITEM()
RATIONAL_B_SPLINE_CURVE((1.,0.965925826289068,1.,0.965925826289068,1.,0.965925826289068,
1.,0.965925826289068,1.,0.965925826289068,1.,0.965925826289068,1.,0.965925826289068,
1.,0.965925826289068,1.,0.965925826289068,1.,0.965925826289068,1.,0.965925826289068,
1.,0.965925826289068,1.,0.965925826289068,1.,0.965925826289068,1.,0.965925826289068,
1.,0.965925826289068,1.,0.965925826289068,1.,0.965925826289068,1.,0.965925826289068,
1.,0.965925826289068,1.,0.965925826289068,1.,0.965925826289068,1.,0.965925826289068,
1.,0.974050567751015,0.98762508931862))
REPRESENTATION_ITEM('')
);
#1888=(
BOUNDED_CURVE()
B_SPLINE_CURVE(2,(#33304,#33305,#33306,#33307,#33308,#33309,#33310,#33311,
#33312,#33313,#33314,#33315,#33316),.UNSPECIFIED.,.F.,.F.)
B_SPLINE_CURVE_WITH_KNOTS((3,2,2,2,2,2,3),(0.,0.0277777777777779,0.0555555555555558,
0.0833333333333336,0.111111111111111,0.138888888888889,0.166666666666668),
 .UNSPECIFIED.)
CURVE()
GEOMETRIC_REPRESENTATION_ITEM()
RATIONAL_B_SPLINE_CURVE((1.,0.965925826289068,1.,0.965925826289068,1.,0.965925826289068,
1.,0.965925826289068,1.,0.965925826289068,1.,0.965925826289068,1.))
REPRESENTATION_ITEM('')
);
#1889=(
BOUNDED_CURVE()
B_SPLINE_CURVE(2,(#33318,#33319,#33320,#33321,#33322,#33323,#33324,#33325,
#33326,#33327,#33328,#33329,#33330),.UNSPECIFIED.,.F.,.F.)
B_SPLINE_CURVE_WITH_KNOTS((3,2,2,2,2,2,3),(0.166666666666668,0.194444444444445,
0.222222222222222,0.25,0.277777777777778,0.305555555555555,0.333333333333333),
 .UNSPECIFIED.)
CURVE()
GEOMETRIC_REPRESENTATION_ITEM()
RATIONAL_B_SPLINE_CURVE((1.,0.965925826289069,1.,0.965925826289068,1.,0.965925826289068,
1.,0.965925826289068,1.,0.965925826289068,1.,0.965925826289069,1.))
REPRESENTATION_ITEM('')
);
#1890=(
BOUNDED_CURVE()
B_SPLINE_CURVE(2,(#33332,#33333,#33334,#33335,#33336,#33337,#33338,#33339,
#33340,#33341,#33342,#33343,#33344),.UNSPECIFIED.,.F.,.F.)
B_SPLINE_CURVE_WITH_KNOTS((3,2,2,2,2,2,3),(0.333333333333333,0.361111111111111,
0.388888888888889,0.416666666666667,0.444444444444444,0.472222222222222,
0.5),.UNSPECIFIED.)
CURVE()
GEOMETRIC_REPRESENTATION_ITEM()
RATIONAL_B_SPLINE_CURVE((1.,0.965925826289068,1.,0.965925826289068,1.,0.965925826289068,
1.,0.965925826289068,1.,0.965925826289068,1.,0.965925826289068,1.))
REPRESENTATION_ITEM('')
);
#1891=(
BOUNDED_CURVE()
B_SPLINE_CURVE(2,(#33346,#33347,#33348,#33349,#33350,#33351,#33352),
 .UNSPECIFIED.,.F.,.F.)
B_SPLINE_CURVE_WITH_KNOTS((3,2,2,3),(0.5,0.527777777777778,0.555555555555556,
0.56047189898401),.UNSPECIFIED.)
CURVE()
GEOMETRIC_REPRESENTATION_ITEM()
RATIONAL_B_SPLINE_CURVE((1.,0.965925826289069,1.,0.965925826289068,1.,0.993969267759865,
0.990073274378594))
REPRESENTATION_ITEM('')
);
#1892=(
BOUNDED_CURVE()
B_SPLINE_CURVE(2,(#33398,#33399,#33400,#33401,#33402),.UNSPECIFIED.,.F.,
 .F.)
B_SPLINE_CURVE_WITH_KNOTS((3,2,3),(0.796543286201692,0.805555555555556,
0.833333333333333),.UNSPECIFIED.)
CURVE()
GEOMETRIC_REPRESENTATION_ITEM()
RATIONAL_B_SPLINE_CURVE((0.985063294131948,0.988944917266243,1.,0.965925826289068,
1.))
REPRESENTATION_ITEM('')
);
#1893=(
BOUNDED_CURVE()
B_SPLINE_CURVE(2,(#33413,#33414,#33415,#33416,#33417,#33418,#33419),
 .UNSPECIFIED.,.F.,.F.)
B_SPLINE_CURVE_WITH_KNOTS((3,2,2,3),(0.77026876316387,0.777777777777778,
0.805555555555556,0.833333333333333),.UNSPECIFIED.)
CURVE()
GEOMETRIC_REPRESENTATION_ITEM()
RATIONAL_B_SPLINE_CURVE((0.986557794578313,0.99078891513932,1.,0.965925826289068,
1.,0.965925826289068,1.))
REPRESENTATION_ITEM('')
);
#2910=ORIENTED_EDGE('',*,*,#6102,.T.);
#2911=ORIENTED_EDGE('',*,*,#6103,.T.);
#2912=ORIENTED_EDGE('',*,*,#6104,.T.);
#2913=ORIENTED_EDGE('',*,*,#6105,.F.);
#2914=ORIENTED_EDGE('',*,*,#6106,.F.);
#2915=ORIENTED_EDGE('',*,*,#6107,.F.);
#2916=ORIENTED_EDGE('',*,*,#6108,.F.);
#2917=ORIENTED_EDGE('',*,*,#6109,.F.);
#2918=ORIENTED_EDGE('',*,*,#6110,.T.);
#2919=ORIENTED_EDGE('',*,*,#6111,.T.);
#2920=ORIENTED_EDGE('',*,*,#6112,.T.);
#2921=ORIENTED_EDGE('',*,*,#6103,.F.);
#2922=ORIENTED_EDGE('',*,*,#6113,.T.);
#2923=ORIENTED_EDGE('',*,*,#6114,.T.);
#2924=ORIENTED_EDGE('',*,*,#6115,.T.);
#2925=ORIENTED_EDGE('',*,*,#6110,.F.);
#2926=ORIENTED_EDGE('',*,*,#6116,.T.);
#2927=ORIENTED_EDGE('',*,*,#6117,.T.);
#2928=ORIENTED_EDGE('',*,*,#6118,.T.);
#2929=ORIENTED_EDGE('',*,*,#6114,.F.);
#2930=ORIENTED_EDGE('',*,*,#6119,.T.);
#2931=ORIENTED_EDGE('',*,*,#6120,.F.);
#2932=ORIENTED_EDGE('',*,*,#6121,.F.);
#2933=ORIENTED_EDGE('',*,*,#6122,.F.);
#2934=ORIENTED_EDGE('',*,*,#6119,.F.);
#2935=ORIENTED_EDGE('',*,*,#6116,.F.);
#2936=ORIENTED_EDGE('',*,*,#6113,.F.);
#2937=ORIENTED_EDGE('',*,*,#6102,.F.);
#2938=ORIENTED_EDGE('',*,*,#6123,.F.);
#2939=ORIENTED_EDGE('',*,*,#6124,.T.);
#2940=ORIENTED_EDGE('',*,*,#6125,.T.);
#2941=ORIENTED_EDGE('',*,*,#6126,.F.);
#2942=ORIENTED_EDGE('',*,*,#6127,.T.);
#2943=ORIENTED_EDGE('',*,*,#6128,.T.);
#2944=ORIENTED_EDGE('',*,*,#6129,.T.);
#2945=ORIENTED_EDGE('',*,*,#6117,.F.);
#2946=ORIENTED_EDGE('',*,*,#6122,.T.);
#2947=ORIENTED_EDGE('',*,*,#6130,.T.);
#2948=ORIENTED_EDGE('',*,*,#6131,.T.);
#2949=ORIENTED_EDGE('',*,*,#6128,.F.);
#2950=ORIENTED_EDGE('',*,*,#6121,.T.);
#2951=ORIENTED_EDGE('',*,*,#6126,.T.);
#2952=ORIENTED_EDGE('',*,*,#6132,.T.);
#2953=ORIENTED_EDGE('',*,*,#6130,.F.);
#2954=ORIENTED_EDGE('',*,*,#6120,.T.);
#2955=ORIENTED_EDGE('',*,*,#6133,.T.);
#2956=ORIENTED_EDGE('',*,*,#6134,.T.);
#2957=ORIENTED_EDGE('',*,*,#6135,.T.);
#2958=ORIENTED_EDGE('',*,*,#6136,.T.);
#2959=ORIENTED_EDGE('',*,*,#6112,.F.);
#2960=ORIENTED_EDGE('',*,*,#6137,.T.);
#2961=ORIENTED_EDGE('',*,*,#6124,.F.);
#2962=ORIENTED_EDGE('',*,*,#6138,.F.);
#2963=ORIENTED_EDGE('',*,*,#6104,.F.);
#2964=ORIENTED_EDGE('',*,*,#6139,.F.);
#2965=ORIENTED_EDGE('',*,*,#6140,.T.);
#2966=ORIENTED_EDGE('',*,*,#6141,.F.);
#2967=ORIENTED_EDGE('',*,*,#6142,.F.);
#2968=ORIENTED_EDGE('',*,*,#6143,.F.);
#2969=ORIENTED_EDGE('',*,*,#6144,.F.);
#2970=ORIENTED_EDGE('',*,*,#6145,.T.);
#2971=ORIENTED_EDGE('',*,*,#6146,.T.);
#2972=ORIENTED_EDGE('',*,*,#6143,.T.);
#2973=ORIENTED_EDGE('',*,*,#6147,.F.);
#2974=ORIENTED_EDGE('',*,*,#6148,.T.);
#2975=ORIENTED_EDGE('',*,*,#6144,.T.);
#2976=ORIENTED_EDGE('',*,*,#6142,.T.);
#2977=ORIENTED_EDGE('',*,*,#6141,.T.);
#2978=ORIENTED_EDGE('',*,*,#6149,.T.);
#2979=ORIENTED_EDGE('',*,*,#6147,.T.);
#2980=ORIENTED_EDGE('',*,*,#6146,.F.);
#2981=ORIENTED_EDGE('',*,*,#6150,.T.);
#2982=ORIENTED_EDGE('',*,*,#6139,.T.);
#2983=ORIENTED_EDGE('',*,*,#6151,.F.);
#2984=ORIENTED_EDGE('',*,*,#6152,.F.);
#2985=ORIENTED_EDGE('',*,*,#6153,.T.);
#2986=ORIENTED_EDGE('',*,*,#6148,.F.);
#2987=ORIENTED_EDGE('',*,*,#6149,.F.);
#2988=ORIENTED_EDGE('',*,*,#6140,.F.);
#2989=ORIENTED_EDGE('',*,*,#6150,.F.);
#2990=ORIENTED_EDGE('',*,*,#6145,.F.);
#2991=ORIENTED_EDGE('',*,*,#6154,.T.);
#2992=ORIENTED_EDGE('',*,*,#6127,.F.);
#2993=ORIENTED_EDGE('',*,*,#6155,.F.);
#2994=ORIENTED_EDGE('',*,*,#6156,.T.);
#2995=ORIENTED_EDGE('',*,*,#6157,.T.);
#2996=ORIENTED_EDGE('',*,*,#6158,.F.);
#2997=ORIENTED_EDGE('',*,*,#6131,.F.);
#2998=ORIENTED_EDGE('',*,*,#6132,.F.);
#2999=ORIENTED_EDGE('',*,*,#6125,.F.);
#3000=ORIENTED_EDGE('',*,*,#6137,.F.);
#3001=ORIENTED_EDGE('',*,*,#6111,.F.);
#3002=ORIENTED_EDGE('',*,*,#6115,.F.);
#3003=ORIENTED_EDGE('',*,*,#6118,.F.);
#3004=ORIENTED_EDGE('',*,*,#6129,.F.);
#3005=ORIENTED_EDGE('',*,*,#6157,.F.);
#3006=ORIENTED_EDGE('',*,*,#6155,.T.);
#3007=ORIENTED_EDGE('',*,*,#6156,.F.);
#3008=ORIENTED_EDGE('',*,*,#6158,.T.);
#3009=ORIENTED_EDGE('',*,*,#6106,.T.);
#3010=ORIENTED_EDGE('',*,*,#6105,.T.);
#3011=ORIENTED_EDGE('',*,*,#6138,.T.);
#3012=ORIENTED_EDGE('',*,*,#6154,.F.);
#3013=ORIENTED_EDGE('',*,*,#6136,.F.);
#3014=ORIENTED_EDGE('',*,*,#6135,.F.);
#3015=ORIENTED_EDGE('',*,*,#6134,.F.);
#3016=ORIENTED_EDGE('',*,*,#6133,.F.);
#3017=ORIENTED_EDGE('',*,*,#6123,.T.);
#3018=ORIENTED_EDGE('',*,*,#6151,.T.);
#3019=ORIENTED_EDGE('',*,*,#6109,.T.);
#3020=ORIENTED_EDGE('',*,*,#6108,.T.);
#3021=ORIENTED_EDGE('',*,*,#6107,.T.);
#3022=ORIENTED_EDGE('',*,*,#6152,.T.);
#3023=ORIENTED_EDGE('',*,*,#6153,.F.);
#6102=EDGE_CURVE('',#7804,#7805,#602,.T.);
#6103=EDGE_CURVE('',#7805,#7806,#1876,.T.);
#6104=EDGE_CURVE('',#7806,#7807,#603,.T.);
#6105=EDGE_CURVE('',#7808,#7807,#1877,.T.);
#6106=EDGE_CURVE('',#7809,#7808,#1878,.T.);
#6107=EDGE_CURVE('',#7810,#7809,#1879,.T.);
#6108=EDGE_CURVE('',#7811,#7810,#1880,.T.);
#6109=EDGE_CURVE('',#7804,#7811,#1881,.T.);
#6110=EDGE_CURVE('',#7812,#7813,#1882,.T.);
#6111=EDGE_CURVE('',#7813,#7814,#1100,.T.);
#6112=EDGE_CURVE('',#7814,#7806,#8892,.T.);
#6113=EDGE_CURVE('',#7805,#7812,#8893,.T.);
#6114=EDGE_CURVE('',#7815,#7816,#1883,.T.);
#6115=EDGE_CURVE('',#7816,#7813,#1101,.T.);
#6116=EDGE_CURVE('',#7812,#7815,#604,.T.);
#6117=EDGE_CURVE('',#7817,#7818,#1884,.T.);
#6118=EDGE_CURVE('',#7818,#7816,#605,.F.);
#6119=EDGE_CURVE('',#7815,#7817,#8894,.T.);
#6120=EDGE_CURVE('',#7819,#7820,#606,.T.);
#6121=EDGE_CURVE('',#7821,#7819,#8895,.T.);
#6122=EDGE_CURVE('',#7817,#7821,#607,.T.);
#6123=EDGE_CURVE('',#7820,#7804,#8896,.T.);
#6124=EDGE_CURVE('',#7822,#7823,#8897,.T.);
#6125=EDGE_CURVE('',#7823,#7824,#608,.T.);
#6126=EDGE_CURVE('',#7825,#7824,#1885,.T.);
#6127=EDGE_CURVE('',#7825,#7822,#609,.T.);
#6128=EDGE_CURVE('',#7821,#7826,#1886,.T.);
#6129=EDGE_CURVE('',#7826,#7818,#1102,.T.);
#6130=EDGE_CURVE('',#7819,#7827,#1887,.T.);
#6131=EDGE_CURVE('',#7827,#7826,#1103,.T.);
#6132=EDGE_CURVE('',#7824,#7827,#1104,.T.);
#6133=EDGE_CURVE('',#7820,#7828,#1888,.T.);
#6134=EDGE_CURVE('',#7828,#7829,#1889,.T.);
#6135=EDGE_CURVE('',#7829,#7830,#1890,.T.);
#6136=EDGE_CURVE('',#7830,#7825,#1891,.T.);
#6137=EDGE_CURVE('',#7814,#7823,#8898,.T.);
#6138=EDGE_CURVE('',#7807,#7822,#8899,.T.);
#6139=EDGE_CURVE('',#7831,#7832,#8900,.T.);
#6140=EDGE_CURVE('',#7831,#7833,#8901,.T.);
#6141=EDGE_CURVE('',#7834,#7833,#1105,.T.);
#6142=EDGE_CURVE('',#7835,#7834,#8902,.T.);
#6143=EDGE_CURVE('',#7832,#7835,#610,.T.);
#6144=EDGE_CURVE('',#7836,#7835,#1892,.T.);
#6145=EDGE_CURVE('',#7836,#7837,#1106,.T.);
#6146=EDGE_CURVE('',#7837,#7832,#1893,.T.);
#6147=EDGE_CURVE('',#7838,#7834,#611,.T.);
#6148=EDGE_CURVE('',#7838,#7836,#1107,.T.);
#6149=EDGE_CURVE('',#7833,#7838,#1108,.T.);
#6150=EDGE_CURVE('',#7837,#7831,#612,.T.);
#6151=EDGE_CURVE('',#7804,#7804,#613,.T.);
#6152=EDGE_CURVE('',#7839,#7839,#614,.T.);
#6153=EDGE_CURVE('',#7840,#7840,#615,.T.);
#6154=EDGE_CURVE('',#7825,#7822,#616,.T.);
#6155=EDGE_CURVE('',#7841,#7841,#617,.T.);
#6156=EDGE_CURVE('',#7842,#7842,#618,.T.);
#6157=EDGE_CURVE('',#7843,#7843,#619,.T.);
#6158=EDGE_CURVE('',#7844,#7844,#620,.T.);
#7804=VERTEX_POINT('',#31967);
#7805=VERTEX_POINT('',#31968);
#7806=VERTEX_POINT('',#32030);
#7807=VERTEX_POINT('',#32032);
#7808=VERTEX_POINT('',#32046);
#7809=VERTEX_POINT('',#32060);
#7810=VERTEX_POINT('',#32074);
#7811=VERTEX_POINT('',#32088);
#7812=VERTEX_POINT('',#32283);
#7813=VERTEX_POINT('',#32284);
#7814=VERTEX_POINT('',#32289);
#7815=VERTEX_POINT('',#32583);
#7816=VERTEX_POINT('',#32584);
#7817=VERTEX_POINT('',#32645);
#7818=VERTEX_POINT('',#32646);
#7819=VERTEX_POINT('',#32651);
#7820=VERTEX_POINT('',#32652);
#7821=VERTEX_POINT('',#32654);
#7822=VERTEX_POINT('',#32659);
#7823=VERTEX_POINT('',#32660);
#7824=VERTEX_POINT('',#32662);
#7825=VERTEX_POINT('',#32670);
#7826=VERTEX_POINT('',#32935);
#7827=VERTEX_POINT('',#33095);
#7828=VERTEX_POINT('',#33317);
#7829=VERTEX_POINT('',#33331);
#7830=VERTEX_POINT('',#33345);
#7831=VERTEX_POINT('',#33358);
#7832=VERTEX_POINT('',#33359);
#7833=VERTEX_POINT('',#33361);
#7834=VERTEX_POINT('',#33366);
#7835=VERTEX_POINT('',#33368);
#7836=VERTEX_POINT('',#33403);
#7837=VERTEX_POINT('',#33412);
#7838=VERTEX_POINT('',#33445);
#7839=VERTEX_POINT('',#33475);
#7840=VERTEX_POINT('',#33478);
#7841=VERTEX_POINT('',#33482);
#7842=VERTEX_POINT('',#33485);
#7843=VERTEX_POINT('',#33488);
#7844=VERTEX_POINT('',#33490);
#8892=LINE('',#32290,#9720);
#8893=LINE('',#32291,#9721);
#8894=LINE('',#32648,#9722);
#8895=LINE('',#32653,#9723);
#8896=LINE('',#32656,#9724);
#8897=LINE('',#32658,#9725);
#8898=LINE('',#33354,#9726);
#8899=LINE('',#33355,#9727);
#8900=LINE('',#33357,#9728);
#8901=LINE('',#33360,#9729);
#8902=LINE('',#33367,#9730);
#9720=VECTOR('',#16414,1.);
#9721=VECTOR('',#16415,1.);
#9722=VECTOR('',#16422,1.);
#9723=VECTOR('',#16427,1.);
#9724=VECTOR('',#16430,1.);
#9725=VECTOR('',#16433,1.);
#9726=VECTOR('',#16440,1.);
#9727=VECTOR('',#16441,1.);
#9728=VECTOR('',#16444,1.);
#9729=VECTOR('',#16445,1.);
#9730=VECTOR('',#16446,1.);
#10811=EDGE_LOOP('',(#2910,#2911,#2912,#2913,#2914,#2915,#2916,#2917));
#10812=EDGE_LOOP('',(#2918,#2919,#2920,#2921,#2922));
#10813=EDGE_LOOP('',(#2923,#2924,#2925,#2926));
#10814=EDGE_LOOP('',(#2927,#2928,#2929,#2930));
#10815=EDGE_LOOP('',(#2931,#2932,#2933,#2934,#2935,#2936,#2937,#2938));
#10816=EDGE_LOOP('',(#2939,#2940,#2941,#2942));
#10817=EDGE_LOOP('',(#2943,#2944,#2945,#2946));
#10818=EDGE_LOOP('',(#2947,#2948,#2949,#2950));
#10819=EDGE_LOOP('',(#2951,#2952,#2953,#2954,#2955,#2956,#2957,#2958));
#10820=EDGE_LOOP('',(#2959,#2960,#2961,#2962,#2963));
#10821=EDGE_LOOP('',(#2964,#2965,#2966,#2967,#2968));
#10822=EDGE_LOOP('',(#2969,#2970,#2971,#2972));
#10823=EDGE_LOOP('',(#2973,#2974,#2975,#2976));
#10824=EDGE_LOOP('',(#2977,#2978,#2979));
#10825=EDGE_LOOP('',(#2980,#2981,#2982));
#10826=EDGE_LOOP('',(#2983));
#10827=EDGE_LOOP('',(#2984));
#10828=EDGE_LOOP('',(#2985));
#10829=EDGE_LOOP('',(#2986,#2987,#2988,#2989,#2990));
#10830=EDGE_LOOP('',(#2991,#2992));
#10831=EDGE_LOOP('',(#2993));
#10832=EDGE_LOOP('',(#2994));
#10833=EDGE_LOOP('',(#2995));
#10834=EDGE_LOOP('',(#2996));
#10835=EDGE_LOOP('',(#2997,#2998,#2999,#3000,#3001,#3002,#3003,#3004));
#10836=EDGE_LOOP('',(#3005));
#10837=EDGE_LOOP('',(#3006));
#10838=EDGE_LOOP('',(#3007));
#10839=EDGE_LOOP('',(#3008));
#10840=EDGE_LOOP('',(#3009,#3010,#3011,#3012,#3013,#3014,#3015,#3016,#3017,
#3018,#3019,#3020,#3021));
#10841=EDGE_LOOP('',(#3022));
#10842=EDGE_LOOP('',(#3023));
#11928=FACE_BOUND('',#10811,.T.);
#11929=FACE_BOUND('',#10812,.T.);
#11930=FACE_BOUND('',#10813,.T.);
#11931=FACE_BOUND('',#10814,.T.);
#11932=FACE_BOUND('',#10815,.T.);
#11933=FACE_BOUND('',#10816,.T.);
#11934=FACE_BOUND('',#10817,.T.);
#11935=FACE_BOUND('',#10818,.T.);
#11936=FACE_BOUND('',#10819,.T.);
#11937=FACE_BOUND('',#10820,.T.);
#11938=FACE_BOUND('',#10821,.T.);
#11939=FACE_BOUND('',#10822,.T.);
#11940=FACE_BOUND('',#10823,.T.);
#11941=FACE_BOUND('',#10824,.T.);
#11942=FACE_BOUND('',#10825,.T.);
#11943=FACE_BOUND('',#10826,.T.);
#11944=FACE_BOUND('',#10827,.T.);
#11945=FACE_BOUND('',#10828,.T.);
#11946=FACE_BOUND('',#10829,.T.);
#11947=FACE_BOUND('',#10830,.T.);
#11948=FACE_BOUND('',#10831,.T.);
#11949=FACE_BOUND('',#10832,.T.);
#11950=FACE_BOUND('',#10833,.T.);
#11951=FACE_BOUND('',#10834,.T.);
#11952=FACE_BOUND('',#10835,.T.);
#11953=FACE_BOUND('',#10836,.T.);
#11954=FACE_BOUND('',#10837,.T.);
#11955=FACE_BOUND('',#10838,.T.);
#11956=FACE_BOUND('',#10839,.T.);
#11957=FACE_BOUND('',#10840,.T.);
#11958=FACE_BOUND('',#10841,.T.);
#11959=FACE_BOUND('',#10842,.T.);
#12676=(
BOUNDED_SURFACE()
B_SPLINE_SURFACE(3,2,((#31722,#31723,#31724,#31725,#31726,#31727,#31728,
#31729,#31730,#31731,#31732,#31733,#31734,#31735,#31736,#31737,#31738,#31739,
#31740,#31741,#31742,#31743,#31744,#31745,#31746,#31747,#31748,#31749,#31750,
#31751,#31752,#31753,#31754,#31755,#31756,#31757,#31758,#31759,#31760,#31761,
#31762,#31763,#31764,#31765,#31766,#31767,#31768,#31769,#31770,#31771,#31772,
#31773,#31774,#31775,#31776,#31777,#31778,#31779,#31780,#31781,#31782),
(#31783,#31784,#31785,#31786,#31787,#31788,#31789,#31790,#31791,#31792,
#31793,#31794,#31795,#31796,#31797,#31798,#31799,#31800,#31801,#31802,#31803,
#31804,#31805,#31806,#31807,#31808,#31809,#31810,#31811,#31812,#31813,#31814,
#31815,#31816,#31817,#31818,#31819,#31820,#31821,#31822,#31823,#31824,#31825,
#31826,#31827,#31828,#31829,#31830,#31831,#31832,#31833,#31834,#31835,#31836,
#31837,#31838,#31839,#31840,#31841,#31842,#31843),(#31844,#31845,#31846,
#31847,#31848,#31849,#31850,#31851,#31852,#31853,#31854,#31855,#31856,#31857,
#31858,#31859,#31860,#31861,#31862,#31863,#31864,#31865,#31866,#31867,#31868,
#31869,#31870,#31871,#31872,#31873,#31874,#31875,#31876,#31877,#31878,#31879,
#31880,#31881,#31882,#31883,#31884,#31885,#31886,#31887,#31888,#31889,#31890,
#31891,#31892,#31893,#31894,#31895,#31896,#31897,#31898,#31899,#31900,#31901,
#31902,#31903,#31904),(#31905,#31906,#31907,#31908,#31909,#31910,#31911,
#31912,#31913,#31914,#31915,#31916,#31917,#31918,#31919,#31920,#31921,#31922,
#31923,#31924,#31925,#31926,#31927,#31928,#31929,#31930,#31931,#31932,#31933,
#31934,#31935,#31936,#31937,#31938,#31939,#31940,#31941,#31942,#31943,#31944,
#31945,#31946,#31947,#31948,#31949,#31950,#31951,#31952,#31953,#31954,#31955,
#31956,#31957,#31958,#31959,#31960,#31961,#31962,#31963,#31964,#31965)),
 .UNSPECIFIED.,.F.,.F.,.F.)
B_SPLINE_SURFACE_WITH_KNOTS((4,4),(3,2,2,2,2,2,2,2,2,2,2,2,2,2,2,2,2,2,
2,2,2,2,2,2,2,2,2,2,2,2,3),(0.,1.),(0.,0.0277777777777778,0.0555555555555556,
0.0833333333333333,0.111111111111111,0.138888888888889,0.166666666666667,
0.194444444444445,0.222222222222222,0.25,0.277777777777778,0.305555555555555,
0.333333333333334,0.361111111111111,0.388888888888889,0.416666666666667,
0.444444444444444,0.472222222222222,0.5,0.527777777777778,0.555555555555556,
0.583333333333333,0.611111111111111,0.638888888888889,0.666666666666667,
0.694444444444444,0.722222222222222,0.75,0.777777777777778,0.805555555555556,
0.833333333333333),.PIECEWISE_BEZIER_KNOTS.)
GEOMETRIC_REPRESENTATION_ITEM()
RATIONAL_B_SPLINE_SURFACE(((1.,0.965925826289068,1.,0.965925826289068,1.,
0.965925826289068,1.,0.965925826289068,1.,0.965925826289068,1.,0.965925826289068,
1.,0.965925826289068,1.,0.965925826289068,1.,0.965925826289068,1.,0.965925826289068,
1.,0.965925826289068,1.,0.965925826289068,1.,0.965925826289068,1.,0.965925826289068,
1.,0.965925826289068,1.,0.965925826289068,1.,0.965925826289068,1.,0.965925826289068,
1.,0.965925826289068,1.,0.965925826289068,1.,0.965925826289068,1.,0.965925826289068,
1.,0.965925826289068,1.,0.965925826289068,1.,0.965925826289068,1.,0.965925826289068,
1.,0.965925826289068,1.,0.965925826289068,1.,0.965925826289068,1.,0.965925826289068,
1.),(0.949253021674191,0.916908009318038,0.949253021674191,0.916908009318038,
0.949253021674191,0.916908009318038,0.949253021674191,0.916908009318038,
0.949253021674191,0.916908009318038,0.949253021674191,0.916908009318038,
0.949253021674191,0.916908009318038,0.949253021674191,0.916908009318038,
0.949253021674191,0.916908009318038,0.949253021674191,0.916908009318038,
0.949253021674191,0.916908009318038,0.949253021674191,0.916908009318038,
0.949253021674191,0.916908009318038,0.949253021674191,0.916908009318038,
0.949253021674191,0.916908009318038,0.949253021674191,0.916908009318038,
0.949253021674191,0.916908009318038,0.949253021674191,0.916908009318038,
0.949253021674191,0.916908009318038,0.949253021674191,0.916908009318038,
0.949253021674191,0.916908009318038,0.949253021674191,0.916908009318038,
0.949253021674191,0.916908009318038,0.949253021674191,0.916908009318038,
0.949253021674191,0.916908009318038,0.949253021674191,0.916908009318038,
0.949253021674191,0.916908009318038,0.949253021674191,0.916908009318038,
0.949253021674191,0.916908009318038,0.949253021674191,0.916908009318038,
0.949253021674191),(0.949253021674191,0.916908009318038,0.949253021674191,
0.916908009318038,0.949253021674191,0.916908009318038,0.949253021674191,
0.916908009318038,0.949253021674191,0.916908009318038,0.949253021674191,
0.916908009318038,0.949253021674191,0.916908009318038,0.949253021674191,
0.916908009318038,0.949253021674191,0.916908009318038,0.949253021674191,
0.916908009318038,0.949253021674191,0.916908009318038,0.949253021674191,
0.916908009318038,0.949253021674191,0.916908009318038,0.949253021674191,
0.916908009318038,0.949253021674191,0.916908009318038,0.949253021674191,
0.916908009318038,0.949253021674191,0.916908009318038,0.949253021674191,
0.916908009318038,0.949253021674191,0.916908009318038,0.949253021674191,
0.916908009318038,0.949253021674191,0.916908009318038,0.949253021674191,
0.916908009318038,0.949253021674191,0.916908009318038,0.949253021674191,
0.916908009318038,0.949253021674191,0.916908009318038,0.949253021674191,
0.916908009318038,0.949253021674191,0.916908009318038,0.949253021674191,
0.916908009318038,0.949253021674191,0.916908009318038,0.949253021674191,
0.916908009318038,0.949253021674191),(1.,0.965925826289068,1.,0.965925826289068,
1.,0.965925826289068,1.,0.965925826289068,1.,0.965925826289068,1.,0.965925826289068,
1.,0.965925826289068,1.,0.965925826289068,1.,0.965925826289068,1.,0.965925826289068,
1.,0.965925826289068,1.,0.965925826289068,1.,0.965925826289068,1.,0.965925826289068,
1.,0.965925826289068,1.,0.965925826289068,1.,0.965925826289068,1.,0.965925826289068,
1.,0.965925826289068,1.,0.965925826289068,1.,0.965925826289068,1.,0.965925826289068,
1.,0.965925826289068,1.,0.965925826289068,1.,0.965925826289068,1.,0.965925826289068,
1.,0.965925826289068,1.,0.965925826289068,1.,0.965925826289068,1.,0.965925826289068,
1.)))
REPRESENTATION_ITEM('')
SURFACE()
);
#12677=(
BOUNDED_SURFACE()
B_SPLINE_SURFACE(1,2,((#32102,#32103,#32104,#32105,#32106,#32107,#32108,
#32109,#32110,#32111,#32112,#32113,#32114,#32115,#32116,#32117,#32118,#32119,
#32120,#32121,#32122,#32123,#32124,#32125,#32126,#32127,#32128,#32129,#32130,
#32131,#32132,#32133,#32134,#32135,#32136,#32137,#32138,#32139,#32140,#32141,
#32142,#32143,#32144,#32145,#32146,#32147,#32148,#32149,#32150,#32151,#32152,
#32153,#32154,#32155,#32156,#32157,#32158,#32159,#32160,#32161,#32162),
(#32163,#32164,#32165,#32166,#32167,#32168,#32169,#32170,#32171,#32172,
#32173,#32174,#32175,#32176,#32177,#32178,#32179,#32180,#32181,#32182,#32183,
#32184,#32185,#32186,#32187,#32188,#32189,#32190,#32191,#32192,#32193,#32194,
#32195,#32196,#32197,#32198,#32199,#32200,#32201,#32202,#32203,#32204,#32205,
#32206,#32207,#32208,#32209,#32210,#32211,#32212,#32213,#32214,#32215,#32216,
#32217,#32218,#32219,#32220,#32221,#32222,#32223)),.RULED_SURF.,.F.,.F.,
 .F.)
B_SPLINE_SURFACE_WITH_KNOTS((2,2),(3,2,2,2,2,2,2,2,2,2,2,2,2,2,2,2,2,2,
2,2,2,2,2,2,2,2,2,2,2,2,3),(0.,1.),(0.,0.0277777777777778,0.0555555555555556,
0.0833333333333333,0.111111111111111,0.138888888888889,0.166666666666667,
0.194444444444445,0.222222222222222,0.25,0.277777777777778,0.305555555555555,
0.333333333333334,0.361111111111111,0.388888888888889,0.416666666666667,
0.444444444444444,0.472222222222222,0.5,0.527777777777778,0.555555555555556,
0.583333333333333,0.611111111111111,0.638888888888889,0.666666666666667,
0.694444444444444,0.722222222222222,0.75,0.777777777777778,0.805555555555556,
0.833333333333333),.UNSPECIFIED.)
GEOMETRIC_REPRESENTATION_ITEM()
RATIONAL_B_SPLINE_SURFACE(((1.,0.965925826289068,1.,0.965925826289068,1.,
0.965925826289068,1.,0.965925826289068,1.,0.965925826289068,1.,0.965925826289068,
1.,0.965925826289068,1.,0.965925826289068,1.,0.965925826289068,1.,0.965925826289068,
1.,0.965925826289068,1.,0.965925826289068,1.,0.965925826289068,1.,0.965925826289068,
1.,0.965925826289068,1.,0.965925826289068,1.,0.965925826289068,1.,0.965925826289068,
1.,0.965925826289068,1.,0.965925826289068,1.,0.965925826289068,1.,0.965925826289068,
1.,0.965925826289068,1.,0.965925826289068,1.,0.965925826289068,1.,0.965925826289068,
1.,0.965925826289068,1.,0.965925826289068,1.,0.965925826289068,1.,0.965925826289068,
1.),(1.,0.965925826289068,1.,0.965925826289068,1.,0.965925826289068,1.,
0.965925826289068,1.,0.965925826289068,1.,0.965925826289068,1.,0.965925826289068,
1.,0.965925826289068,1.,0.965925826289068,1.,0.965925826289068,1.,0.965925826289068,
1.,0.965925826289068,1.,0.965925826289068,1.,0.965925826289068,1.,0.965925826289068,
1.,0.965925826289068,1.,0.965925826289068,1.,0.965925826289068,1.,0.965925826289068,
1.,0.965925826289068,1.,0.965925826289068,1.,0.965925826289068,1.,0.965925826289068,
1.,0.965925826289068,1.,0.965925826289068,1.,0.965925826289068,1.,0.965925826289068,
1.,0.965925826289068,1.,0.965925826289068,1.,0.965925826289068,1.)))
REPRESENTATION_ITEM('')
SURFACE()
);
#12678=(
BOUNDED_SURFACE()
B_SPLINE_SURFACE(3,2,((#32292,#32293,#32294,#32295,#32296,#32297,#32298,
#32299,#32300,#32301,#32302,#32303,#32304,#32305,#32306,#32307,#32308,#32309,
#32310,#32311,#32312,#32313,#32314,#32315,#32316,#32317,#32318,#32319,#32320,
#32321,#32322,#32323,#32324,#32325,#32326,#32327,#32328,#32329,#32330,#32331,
#32332,#32333,#32334,#32335,#32336,#32337,#32338,#32339,#32340,#32341,#32342,
#32343,#32344,#32345,#32346,#32347,#32348,#32349,#32350),(#32351,#32352,
#32353,#32354,#32355,#32356,#32357,#32358,#32359,#32360,#32361,#32362,#32363,
#32364,#32365,#32366,#32367,#32368,#32369,#32370,#32371,#32372,#32373,#32374,
#32375,#32376,#32377,#32378,#32379,#32380,#32381,#32382,#32383,#32384,#32385,
#32386,#32387,#32388,#32389,#32390,#32391,#32392,#32393,#32394,#32395,#32396,
#32397,#32398,#32399,#32400,#32401,#32402,#32403,#32404,#32405,#32406,#32407,
#32408,#32409),(#32410,#32411,#32412,#32413,#32414,#32415,#32416,#32417,
#32418,#32419,#32420,#32421,#32422,#32423,#32424,#32425,#32426,#32427,#32428,
#32429,#32430,#32431,#32432,#32433,#32434,#32435,#32436,#32437,#32438,#32439,
#32440,#32441,#32442,#32443,#32444,#32445,#32446,#32447,#32448,#32449,#32450,
#32451,#32452,#32453,#32454,#32455,#32456,#32457,#32458,#32459,#32460,#32461,
#32462,#32463,#32464,#32465,#32466,#32467,#32468),(#32469,#32470,#32471,
#32472,#32473,#32474,#32475,#32476,#32477,#32478,#32479,#32480,#32481,#32482,
#32483,#32484,#32485,#32486,#32487,#32488,#32489,#32490,#32491,#32492,#32493,
#32494,#32495,#32496,#32497,#32498,#32499,#32500,#32501,#32502,#32503,#32504,
#32505,#32506,#32507,#32508,#32509,#32510,#32511,#32512,#32513,#32514,#32515,
#32516,#32517,#32518,#32519,#32520,#32521,#32522,#32523,#32524,#32525,#32526,
#32527)),.UNSPECIFIED.,.F.,.F.,.F.)
B_SPLINE_SURFACE_WITH_KNOTS((4,4),(3,2,2,2,2,2,2,2,2,2,2,2,2,2,2,2,2,2,
2,2,2,2,2,2,2,2,2,2,2,3),(0.,1.),(0.,0.0277777777777778,0.0555555555555556,
0.0833333333333333,0.111111111111111,0.138888888888889,0.166666666666667,
0.194444444444445,0.222222222222222,0.25,0.277777777777778,0.305555555555555,
0.333333333333334,0.361111111111111,0.388888888888889,0.416666666666667,
0.444444444444444,0.472222222222222,0.5,0.527777777777778,0.555555555555556,
0.583333333333333,0.611111111111111,0.638888888888889,0.666666666666667,
0.694444444444444,0.722222222222222,0.75,0.777777777777778,0.796430048543053),
 .PIECEWISE_BEZIER_KNOTS.)
GEOMETRIC_REPRESENTATION_ITEM()
RATIONAL_B_SPLINE_SURFACE(((1.,0.965925826289068,1.,0.965925826289068,1.,
0.965925826289068,1.,0.965925826289068,1.,0.965925826289068,1.,0.965925826289068,
1.,0.965925826289068,1.,0.965925826289068,1.,0.965925826289068,1.,0.965925826289068,
1.,0.965925826289068,1.,0.965925826289068,1.,0.965925826289068,1.,0.965925826289068,
1.,0.965925826289068,1.,0.965925826289068,1.,0.965925826289068,1.,0.965925826289068,
1.,0.965925826289068,1.,0.965925826289068,1.,0.965925826289068,1.,0.965925826289068,
1.,0.965925826289068,1.,0.965925826289068,1.,0.965925826289068,1.,0.965925826289068,
1.,0.965925826289068,1.,0.965925826289068,1.,0.977119814290265,0.984966882749808),
(0.949253021674191,0.916908009318038,0.949253021674191,0.916908009318038,
0.949253021674191,0.916908009318038,0.949253021674191,0.916908009318038,
0.949253021674191,0.916908009318038,0.949253021674191,0.916908009318038,
0.949253021674191,0.916908009318038,0.949253021674191,0.916908009318038,
0.949253021674191,0.916908009318038,0.949253021674191,0.916908009318038,
0.949253021674191,0.916908009318038,0.949253021674191,0.916908009318038,
0.949253021674191,0.916908009318038,0.949253021674191,0.916908009318038,
0.949253021674191,0.916908009318038,0.949253021674191,0.916908009318038,
0.949253021674191,0.916908009318038,0.949253021674191,0.916908009318038,
0.949253021674191,0.916908009318038,0.949253021674191,0.916908009318038,
0.949253021674191,0.916908009318038,0.949253021674191,0.916908009318038,
0.949253021674191,0.916908009318038,0.949253021674191,0.916908009318038,
0.949253021674191,0.916908009318038,0.949253021674191,0.916908009318038,
0.949253021674191,0.916908009318038,0.949253021674191,0.916908009318038,
0.949253021674191,0.927533936252759,0.934982789699264),(0.949253021674191,
0.916908009318038,0.949253021674191,0.916908009318038,0.949253021674191,
0.916908009318038,0.949253021674191,0.916908009318038,0.949253021674191,
0.916908009318038,0.949253021674191,0.916908009318038,0.949253021674191,
0.916908009318038,0.949253021674191,0.916908009318038,0.949253021674191,
0.916908009318038,0.949253021674191,0.916908009318038,0.949253021674191,
0.916908009318038,0.949253021674191,0.916908009318038,0.949253021674191,
0.916908009318038,0.949253021674191,0.916908009318038,0.949253021674191,
0.916908009318038,0.949253021674191,0.916908009318038,0.949253021674191,
0.916908009318038,0.949253021674191,0.916908009318038,0.949253021674191,
0.916908009318038,0.949253021674191,0.916908009318038,0.949253021674191,
0.916908009318038,0.949253021674191,0.916908009318038,0.949253021674191,
0.916908009318038,0.949253021674191,0.916908009318038,0.949253021674191,
0.916908009318038,0.949253021674191,0.916908009318038,0.949253021674191,
0.916908009318038,0.949253021674191,0.916908009318038,0.949253021674191,
0.927533936252759,0.934982789699264),(1.,0.965925826289068,1.,0.965925826289068,
1.,0.965925826289068,1.,0.965925826289068,1.,0.965925826289068,1.,0.965925826289068,
1.,0.965925826289068,1.,0.965925826289068,1.,0.965925826289068,1.,0.965925826289068,
1.,0.965925826289068,1.,0.965925826289068,1.,0.965925826289068,1.,0.965925826289068,
1.,0.965925826289068,1.,0.965925826289068,1.,0.965925826289068,1.,0.965925826289068,
1.,0.965925826289068,1.,0.965925826289068,1.,0.965925826289068,1.,0.965925826289068,
1.,0.965925826289068,1.,0.965925826289068,1.,0.965925826289068,1.,0.965925826289068,
1.,0.965925826289068,1.,0.965925826289068,1.,0.977119814290265,0.984966882749808)))
REPRESENTATION_ITEM('')
SURFACE()
);
#12679=(
BOUNDED_SURFACE()
B_SPLINE_SURFACE(3,2,((#32672,#32673,#32674,#32675,#32676,#32677,#32678,
#32679,#32680,#32681,#32682,#32683,#32684,#32685,#32686,#32687,#32688,#32689,
#32690,#32691,#32692,#32693,#32694,#32695,#32696,#32697,#32698,#32699,#32700,
#32701,#32702,#32703,#32704,#32705,#32706,#32707,#32708,#32709,#32710,#32711,
#32712,#32713,#32714,#32715,#32716,#32717,#32718,#32719,#32720,#32721,#32722,
#32723,#32724),(#32725,#32726,#32727,#32728,#32729,#32730,#32731,#32732,
#32733,#32734,#32735,#32736,#32737,#32738,#32739,#32740,#32741,#32742,#32743,
#32744,#32745,#32746,#32747,#32748,#32749,#32750,#32751,#32752,#32753,#32754,
#32755,#32756,#32757,#32758,#32759,#32760,#32761,#32762,#32763,#32764,#32765,
#32766,#32767,#32768,#32769,#32770,#32771,#32772,#32773,#32774,#32775,#32776,
#32777),(#32778,#32779,#32780,#32781,#32782,#32783,#32784,#32785,#32786,
#32787,#32788,#32789,#32790,#32791,#32792,#32793,#32794,#32795,#32796,#32797,
#32798,#32799,#32800,#32801,#32802,#32803,#32804,#32805,#32806,#32807,#32808,
#32809,#32810,#32811,#32812,#32813,#32814,#32815,#32816,#32817,#32818,#32819,
#32820,#32821,#32822,#32823,#32824,#32825,#32826,#32827,#32828,#32829,#32830),
(#32831,#32832,#32833,#32834,#32835,#32836,#32837,#32838,#32839,#32840,
#32841,#32842,#32843,#32844,#32845,#32846,#32847,#32848,#32849,#32850,#32851,
#32852,#32853,#32854,#32855,#32856,#32857,#32858,#32859,#32860,#32861,#32862,
#32863,#32864,#32865,#32866,#32867,#32868,#32869,#32870,#32871,#32872,#32873,
#32874,#32875,#32876,#32877,#32878,#32879,#32880,#32881,#32882,#32883)),
 .UNSPECIFIED.,.F.,.F.,.F.)
B_SPLINE_SURFACE_WITH_KNOTS((4,4),(3,2,2,2,2,2,2,2,2,2,2,2,2,2,2,2,2,2,
2,2,2,2,2,2,2,2,3),(0.,1.),(0.,0.0277777777777778,0.0555555555555556,0.0833333333333333,
0.111111111111111,0.138888888888889,0.166666666666667,0.194444444444445,
0.222222222222222,0.25,0.277777777777778,0.305555555555555,0.333333333333334,
0.361111111111111,0.388888888888889,0.416666666666667,0.444444444444444,
0.472222222222222,0.5,0.527777777777778,0.555555555555556,0.583333333333333,
0.611111111111111,0.638888888888889,0.666666666666667,0.694444444444444,
0.702647985953411),.PIECEWISE_BEZIER_KNOTS.)
GEOMETRIC_REPRESENTATION_ITEM()
RATIONAL_B_SPLINE_SURFACE(((1.,0.965925826289068,1.,0.965925826289068,1.,
0.965925826289068,1.,0.965925826289068,1.,0.965925826289068,1.,0.965925826289068,
1.,0.965925826289068,1.,0.965925826289068,1.,0.965925826289068,1.,0.965925826289068,
1.,0.965925826289068,1.,0.965925826289068,1.,0.965925826289068,1.,0.965925826289068,
1.,0.965925826289068,1.,0.965925826289068,1.,0.965925826289068,1.,0.965925826289068,
1.,0.965925826289068,1.,0.965925826289068,1.,0.965925826289068,1.,0.965925826289068,
1.,0.965925826289068,1.,0.965925826289068,1.,0.965925826289068,1.,0.98993695965683,
0.985817704293295),(0.844029628745982,0.815270016558918,0.844029628745982,
0.815270016558918,0.844029628745982,0.815270016558918,0.844029628745982,
0.815270016558918,0.844029628745982,0.815270016558918,0.844029628745982,
0.815270016558918,0.844029628745982,0.815270016558918,0.844029628745982,
0.815270016558918,0.844029628745982,0.815270016558918,0.844029628745982,
0.815270016558918,0.844029628745982,0.815270016558918,0.844029628745982,
0.815270016558918,0.844029628745982,0.815270016558918,0.844029628745982,
0.815270016558918,0.844029628745982,0.815270016558918,0.844029628745982,
0.815270016558918,0.844029628745982,0.815270016558918,0.844029628745982,
0.815270016558918,0.844029628745982,0.815270016558918,0.844029628745982,
0.815270016558918,0.844029628745982,0.815270016558918,0.844029628745982,
0.815270016558918,0.844029628745982,0.815270016558918,0.844029628745982,
0.815270016558918,0.844029628745982,0.815270016558918,0.844029628745982,
0.83553612454108,0.832059350965886),(0.844029628745982,0.815270016558918,
0.844029628745982,0.815270016558918,0.844029628745982,0.815270016558918,
0.844029628745982,0.815270016558918,0.844029628745982,0.815270016558918,
0.844029628745982,0.815270016558918,0.844029628745982,0.815270016558918,
0.844029628745982,0.815270016558918,0.844029628745982,0.815270016558918,
0.844029628745982,0.815270016558918,0.844029628745982,0.815270016558918,
0.844029628745982,0.815270016558918,0.844029628745982,0.815270016558918,
0.844029628745982,0.815270016558918,0.844029628745982,0.815270016558918,
0.844029628745982,0.815270016558918,0.844029628745982,0.815270016558918,
0.844029628745982,0.815270016558918,0.844029628745982,0.815270016558918,
0.844029628745982,0.815270016558918,0.844029628745982,0.815270016558918,
0.844029628745982,0.815270016558918,0.844029628745982,0.815270016558918,
0.844029628745982,0.815270016558918,0.844029628745982,0.815270016558918,
0.844029628745982,0.83553612454108,0.832059350965886),(1.,0.965925826289068,
1.,0.965925826289068,1.,0.965925826289068,1.,0.965925826289068,1.,0.965925826289068,
1.,0.965925826289068,1.,0.965925826289068,1.,0.965925826289068,1.,0.965925826289068,
1.,0.965925826289068,1.,0.965925826289068,1.,0.965925826289068,1.,0.965925826289068,
1.,0.965925826289068,1.,0.965925826289068,1.,0.965925826289068,1.,0.965925826289068,
1.,0.965925826289068,1.,0.965925826289068,1.,0.965925826289068,1.,0.965925826289068,
1.,0.965925826289068,1.,0.965925826289068,1.,0.965925826289068,1.,0.965925826289068,
1.,0.98993695965683,0.985817704293295)))
REPRESENTATION_ITEM('')
SURFACE()
);
#12680=(
BOUNDED_SURFACE()
B_SPLINE_SURFACE(1,2,((#32944,#32945,#32946,#32947,#32948,#32949,#32950,
#32951,#32952,#32953,#32954,#32955,#32956,#32957,#32958,#32959,#32960,#32961,
#32962,#32963,#32964,#32965,#32966,#32967,#32968,#32969,#32970,#32971,#32972,
#32973,#32974,#32975,#32976,#32977,#32978,#32979,#32980,#32981,#32982,#32983,
#32984,#32985,#32986,#32987,#32988,#32989,#32990,#32991,#32992,#32993,#32994),
(#32995,#32996,#32997,#32998,#32999,#33000,#33001,#33002,#33003,#33004,
#33005,#33006,#33007,#33008,#33009,#33010,#33011,#33012,#33013,#33014,#33015,
#33016,#33017,#33018,#33019,#33020,#33021,#33022,#33023,#33024,#33025,#33026,
#33027,#33028,#33029,#33030,#33031,#33032,#33033,#33034,#33035,#33036,#33037,
#33038,#33039,#33040,#33041,#33042,#33043,#33044,#33045)),.RULED_SURF.,
 .F.,.F.,.F.)
B_SPLINE_SURFACE_WITH_KNOTS((2,2),(3,2,2,2,2,2,2,2,2,2,2,2,2,2,2,2,2,2,
2,2,2,2,2,2,2,3),(0.,1.),(0.,0.0277777777777778,0.0555555555555556,0.0833333333333333,
0.111111111111111,0.138888888888889,0.166666666666667,0.194444444444445,
0.222222222222222,0.25,0.277777777777778,0.305555555555555,0.333333333333334,
0.361111111111111,0.388888888888889,0.416666666666667,0.444444444444444,
0.472222222222222,0.5,0.527777777777778,0.555555555555556,0.583333333333333,
0.611111111111111,0.638888888888889,0.666666666666667,0.67623687285605),
 .PIECEWISE_BEZIER_KNOTS.)
GEOMETRIC_REPRESENTATION_ITEM()
RATIONAL_B_SPLINE_SURFACE(((1.,0.965925826289068,1.,0.965925826289068,1.,
0.965925826289068,1.,0.965925826289068,1.,0.965925826289068,1.,0.965925826289068,
1.,0.965925826289068,1.,0.965925826289068,1.,0.965925826289068,1.,0.965925826289068,
1.,0.965925826289068,1.,0.965925826289068,1.,0.965925826289068,1.,0.965925826289068,
1.,0.965925826289068,1.,0.965925826289068,1.,0.965925826289068,1.,0.965925826289068,
1.,0.965925826289068,1.,0.965925826289068,1.,0.965925826289068,1.,0.965925826289068,
1.,0.965925826289068,1.,0.965925826289068,1.,0.988260512746727,0.984610176070599),
(1.,0.965925826289068,1.,0.965925826289068,1.,0.965925826289068,1.,0.965925826289068,
1.,0.965925826289068,1.,0.965925826289068,1.,0.965925826289068,1.,0.965925826289068,
1.,0.965925826289068,1.,0.965925826289068,1.,0.965925826289068,1.,0.965925826289068,
1.,0.965925826289068,1.,0.965925826289068,1.,0.965925826289068,1.,0.965925826289068,
1.,0.965925826289068,1.,0.965925826289068,1.,0.965925826289068,1.,0.965925826289068,
1.,0.965925826289068,1.,0.965925826289068,1.,0.965925826289068,1.,0.965925826289068,
1.,0.988260512746727,0.984610176070599)))
REPRESENTATION_ITEM('')
SURFACE()
);
#12681=(
BOUNDED_SURFACE()
B_SPLINE_SURFACE(3,2,((#33100,#33101,#33102,#33103,#33104,#33105,#33106,
#33107,#33108,#33109,#33110,#33111,#33112,#33113,#33114,#33115,#33116,#33117,
#33118,#33119,#33120,#33121,#33122,#33123,#33124,#33125,#33126,#33127,#33128,
#33129,#33130,#33131,#33132,#33133,#33134,#33135,#33136,#33137,#33138,#33139,
#33140,#33141,#33142,#33143,#33144,#33145,#33146,#33147,#33148),(#33149,
#33150,#33151,#33152,#33153,#33154,#33155,#33156,#33157,#33158,#33159,#33160,
#33161,#33162,#33163,#33164,#33165,#33166,#33167,#33168,#33169,#33170,#33171,
#33172,#33173,#33174,#33175,#33176,#33177,#33178,#33179,#33180,#33181,#33182,
#33183,#33184,#33185,#33186,#33187,#33188,#33189,#33190,#33191,#33192,#33193,
#33194,#33195,#33196,#33197),(#33198,#33199,#33200,#33201,#33202,#33203,
#33204,#33205,#33206,#33207,#33208,#33209,#33210,#33211,#33212,#33213,#33214,
#33215,#33216,#33217,#33218,#33219,#33220,#33221,#33222,#33223,#33224,#33225,
#33226,#33227,#33228,#33229,#33230,#33231,#33232,#33233,#33234,#33235,#33236,
#33237,#33238,#33239,#33240,#33241,#33242,#33243,#33244,#33245,#33246),
(#33247,#33248,#33249,#33250,#33251,#33252,#33253,#33254,#33255,#33256,
#33257,#33258,#33259,#33260,#33261,#33262,#33263,#33264,#33265,#33266,#33267,
#33268,#33269,#33270,#33271,#33272,#33273,#33274,#33275,#33276,#33277,#33278,
#33279,#33280,#33281,#33282,#33283,#33284,#33285,#33286,#33287,#33288,#33289,
#33290,#33291,#33292,#33293,#33294,#33295)),.UNSPECIFIED.,.F.,.F.,.F.)
B_SPLINE_SURFACE_WITH_KNOTS((4,4),(3,2,2,2,2,2,2,2,2,2,2,2,2,2,2,2,2,2,
2,2,2,2,2,2,3),(0.,1.),(0.,0.0277777777777778,0.0555555555555556,0.0833333333333333,
0.111111111111111,0.138888888888889,0.166666666666667,0.194444444444445,
0.222222222222222,0.25,0.277777777777778,0.305555555555555,0.333333333333334,
0.361111111111111,0.388888888888889,0.416666666666667,0.444444444444444,
0.472222222222222,0.5,0.527777777777778,0.555555555555556,0.583333333333333,
0.611111111111111,0.638888888888889,0.664003515027687),
 .PIECEWISE_BEZIER_KNOTS.)
GEOMETRIC_REPRESENTATION_ITEM()
RATIONAL_B_SPLINE_SURFACE(((1.,0.965925826289068,1.,0.965925826289068,1.,
0.965925826289068,1.,0.965925826289068,1.,0.965925826289068,1.,0.965925826289068,
1.,0.965925826289068,1.,0.965925826289068,1.,0.965925826289068,1.,0.965925826289068,
1.,0.965925826289068,1.,0.965925826289068,1.,0.965925826289068,1.,0.965925826289068,
1.,0.965925826289068,1.,0.965925826289068,1.,0.965925826289068,1.,0.965925826289068,
1.,0.965925826289068,1.,0.965925826289068,1.,0.965925826289068,1.,0.965925826289068,
1.,0.965925826289068,1.,0.969192635185413,0.9940927827449),(0.844029628745984,
0.81527001655892,0.844029628745984,0.81527001655892,0.844029628745984,0.81527001655892,
0.844029628745984,0.81527001655892,0.844029628745984,0.81527001655892,0.844029628745984,
0.81527001655892,0.844029628745984,0.81527001655892,0.844029628745984,0.81527001655892,
0.844029628745984,0.81527001655892,0.844029628745984,0.81527001655892,0.844029628745984,
0.81527001655892,0.844029628745984,0.81527001655892,0.844029628745984,0.81527001655892,
0.844029628745984,0.81527001655892,0.844029628745984,0.81527001655892,0.844029628745984,
0.81527001655892,0.844029628745984,0.81527001655892,0.844029628745984,0.81527001655892,
0.844029628745984,0.81527001655892,0.844029628745984,0.81527001655892,0.844029628745984,
0.81527001655892,0.844029628745984,0.81527001655892,0.844029628745984,0.81527001655892,
0.844029628745984,0.818027300058886,0.83904376235924),(0.844029628745984,
0.81527001655892,0.844029628745984,0.81527001655892,0.844029628745984,0.81527001655892,
0.844029628745984,0.81527001655892,0.844029628745984,0.81527001655892,0.844029628745984,
0.81527001655892,0.844029628745984,0.81527001655892,0.844029628745984,0.81527001655892,
0.844029628745984,0.81527001655892,0.844029628745984,0.81527001655892,0.844029628745984,
0.81527001655892,0.844029628745984,0.81527001655892,0.844029628745984,0.81527001655892,
0.844029628745984,0.81527001655892,0.844029628745984,0.81527001655892,0.844029628745984,
0.81527001655892,0.844029628745984,0.81527001655892,0.844029628745984,0.81527001655892,
0.844029628745984,0.81527001655892,0.844029628745984,0.81527001655892,0.844029628745984,
0.81527001655892,0.844029628745984,0.81527001655892,0.844029628745984,0.81527001655892,
0.844029628745984,0.818027300058886,0.83904376235924),(1.,0.965925826289068,
1.,0.965925826289068,1.,0.965925826289068,1.,0.965925826289068,1.,0.965925826289068,
1.,0.965925826289068,1.,0.965925826289068,1.,0.965925826289068,1.,0.965925826289068,
1.,0.965925826289068,1.,0.965925826289068,1.,0.965925826289068,1.,0.965925826289068,
1.,0.965925826289068,1.,0.965925826289068,1.,0.965925826289068,1.,0.965925826289068,
1.,0.965925826289068,1.,0.965925826289068,1.,0.965925826289068,1.,0.965925826289068,
1.,0.965925826289068,1.,0.965925826289068,1.,0.969192635185413,0.9940927827449)))
REPRESENTATION_ITEM('')
SURFACE()
);
#12682=(
BOUNDED_SURFACE()
B_SPLINE_SURFACE(3,2,((#33370,#33371,#33372,#33373,#33374,#33375,#33376),
(#33377,#33378,#33379,#33380,#33381,#33382,#33383),(#33384,#33385,#33386,
#33387,#33388,#33389,#33390),(#33391,#33392,#33393,#33394,#33395,#33396,
#33397)),.UNSPECIFIED.,.F.,.F.,.F.)
B_SPLINE_SURFACE_WITH_KNOTS((4,4),(3,2,2,3),(0.,1.),(0.769890375742853,
0.777777777777778,0.805555555555556,0.833333333333333),
 .PIECEWISE_BEZIER_KNOTS.)
GEOMETRIC_REPRESENTATION_ITEM()
RATIONAL_B_SPLINE_SURFACE(((0.986144018469014,0.990324758545624,1.,0.965925826289068,
1.,0.965925826289068,1.),(0.832334769798475,0.83586343829322,0.844029628745984,
0.81527001655892,0.844029628745984,0.81527001655892,0.844029628745984),
(0.832334769798475,0.83586343829322,0.844029628745984,0.81527001655892,
0.844029628745984,0.81527001655892,0.844029628745984),(0.986144018469014,
0.990324758545624,1.,0.965925826289068,1.,0.965925826289068,1.)))
REPRESENTATION_ITEM('')
SURFACE()
);
#12683=(
BOUNDED_SURFACE()
B_SPLINE_SURFACE(3,2,((#33450,#33451,#33452),(#33453,#33454,#33455),(#33456,
#33457,#33458),(#33459,#33460,#33461)),.UNSPECIFIED.,.F.,.F.,.F.)
B_SPLINE_SURFACE_WITH_KNOTS((4,4),(3,3),(0.0382659980764476,1.),(0.808520334142405,
0.833333333333333),.PIECEWISE_BEZIER_KNOTS.)
GEOMETRIC_REPRESENTATION_ITEM()
RATIONAL_B_SPLINE_SURFACE(((0.976394668876932,0.952866831529329,0.982780070198817),
(0.83877262990258,0.818561022202317,0.844258014071977),(0.844475312244286,
0.824126289022556,0.849997990672371),(0.99350271590205,0.969562631990048,
1.)))
REPRESENTATION_ITEM('')
SURFACE()
);
#12954=ADVANCED_FACE('',(#11928),#12676,.T.);
#12955=ADVANCED_FACE('',(#11929),#12677,.T.);
#12956=ADVANCED_FACE('',(#11930),#12678,.T.);
#12957=ADVANCED_FACE('',(#11931),#1624,.F.);
#12958=ADVANCED_FACE('',(#11932),#1278,.F.);
#12959=ADVANCED_FACE('',(#11933),#1625,.T.);
#12960=ADVANCED_FACE('',(#11934),#12679,.T.);
#12961=ADVANCED_FACE('',(#11935),#12680,.T.);
#12962=ADVANCED_FACE('',(#11936),#12681,.T.);
#12963=ADVANCED_FACE('',(#11937),#1279,.F.);
#12964=ADVANCED_FACE('',(#11938),#1280,.F.);
#12965=ADVANCED_FACE('',(#11939),#12682,.T.);
#12966=ADVANCED_FACE('',(#11940),#54,.T.);
#12967=ADVANCED_FACE('',(#11941),#12683,.T.);
#12968=ADVANCED_FACE('',(#11942),#1626,.T.);
#12969=ADVANCED_FACE('',(#11943,#11944),#1281,.F.);
#12970=ADVANCED_FACE('',(#11945,#11946),#1282,.T.);
#12971=ADVANCED_FACE('',(#11947,#11948),#1283,.T.);
#12972=ADVANCED_FACE('',(#11949),#1284,.F.);
#12973=ADVANCED_FACE('',(#11950,#11951,#11952),#1285,.T.);
#12974=ADVANCED_FACE('',(#11953,#11954),#1627,.F.);
#12975=ADVANCED_FACE('',(#11955,#11956),#1628,.T.);
#12976=ADVANCED_FACE('',(#11957),#1629,.F.);
#12977=ADVANCED_FACE('',(#11958,#11959),#1630,.T.);
#13511=CLOSED_SHELL('',(#12954,#12955,#12956,#12957,#12958,#12959,#12960,
#12961,#12962,#12963,#12964,#12965,#12966,#12967,#12968,#12969,#12970,#12971,
#12972,#12973,#12974,#12975,#12976,#12977));
#13538=STYLED_ITEM('',(#13565),#13728);
#13565=PRESENTATION_STYLE_ASSIGNMENT((#13592));
#13592=SURFACE_STYLE_USAGE(.BOTH.,#13619);
#13619=SURFACE_SIDE_STYLE('',(#13646));
#13646=SURFACE_STYLE_FILL_AREA(#13673);
#13673=FILL_AREA_STYLE('',(#13700));
#13700=FILL_AREA_STYLE_COLOUR('',#60);
#13728=MANIFOLD_SOLID_BREP('refill_cap',#13511);
#13756=SHAPE_DEFINITION_REPRESENTATION(#45544,#13784);
#13784=SHAPE_REPRESENTATION('refill_cap',(#13802),#45474);
#13802=AXIS2_PLACEMENT_3D('',#19109,#15295,#15296);
#14300=AXIS2_PLACEMENT_3D('',#31966,#16410,#16411);
#14301=AXIS2_PLACEMENT_3D('',#32031,#16412,#16413);
#14302=AXIS2_PLACEMENT_3D('',#32590,#16416,#16417);
#14303=AXIS2_PLACEMENT_3D('',#32591,#16418,#16419);
#14304=AXIS2_PLACEMENT_3D('',#32647,#16420,#16421);
#14305=AXIS2_PLACEMENT_3D('',#32649,#16423,#16424);
#14306=AXIS2_PLACEMENT_3D('',#32650,#16425,#16426);
#14307=AXIS2_PLACEMENT_3D('',#32655,#16428,#16429);
#14308=AXIS2_PLACEMENT_3D('',#32657,#16431,#16432);
#14309=AXIS2_PLACEMENT_3D('',#32661,#16434,#16435);
#14310=AXIS2_PLACEMENT_3D('',#32671,#16436,#16437);
#14311=AXIS2_PLACEMENT_3D('',#33353,#16438,#16439);
#14312=AXIS2_PLACEMENT_3D('',#33356,#16442,#16443);
#14313=AXIS2_PLACEMENT_3D('',#33369,#16447,#16448);
#14314=AXIS2_PLACEMENT_3D('',#33444,#16449,#16450);
#14315=AXIS2_PLACEMENT_3D('',#33470,#16451,#16452);
#14316=AXIS2_PLACEMENT_3D('',#33471,#16453,#16454);
#14317=AXIS2_PLACEMENT_3D('',#33472,#16455,#16456);
#14318=AXIS2_PLACEMENT_3D('',#33473,#16457,#16458);
#14319=AXIS2_PLACEMENT_3D('',#33474,#16459,#16460);
#14320=AXIS2_PLACEMENT_3D('',#33476,#16461,#16462);
#14321=AXIS2_PLACEMENT_3D('',#33477,#16463,#16464);
#14322=AXIS2_PLACEMENT_3D('',#33479,#16465,#16466);
#14323=AXIS2_PLACEMENT_3D('',#33480,#16467,#16468);
#14324=AXIS2_PLACEMENT_3D('',#33481,#16469,#16470);
#14325=AXIS2_PLACEMENT_3D('',#33483,#16471,#16472);
#14326=AXIS2_PLACEMENT_3D('',#33484,#16473,#16474);
#14327=AXIS2_PLACEMENT_3D('',#33486,#16475,#16476);
#14328=AXIS2_PLACEMENT_3D('',#33487,#16477,#16478);
#14329=AXIS2_PLACEMENT_3D('',#33489,#16479,#16480);
#14330=AXIS2_PLACEMENT_3D('',#33491,#16481,#16482);
#14331=AXIS2_PLACEMENT_3D('',#33492,#16483,#16484);
#14332=AXIS2_PLACEMENT_3D('',#33493,#16485,#16486);
#14333=AXIS2_PLACEMENT_3D('',#33494,#16487,#16488);
#15295=DIRECTION('',(0.,0.,1.));
#15296=DIRECTION('',(1.,0.,0.));
#16410=DIRECTION('',(0.,-1.,0.));
#16411=DIRECTION('',(1.,4.55307998944049E-15,0.));
#16412=DIRECTION('',(1.69409931514E-14,-1.,-1.69409931514E-14));
#16413=DIRECTION('',(-0.707106781186545,-1.82123199577605E-14,0.70710678118655));
#16414=DIRECTION('',(-0.707106781186548,-6.69019751772657E-12,-0.707106781186548));
#16415=DIRECTION('',(-0.707106781186549,-7.90827833040412E-15,0.707106781186547));
#16416=DIRECTION('',(4.08991754261793E-14,1.,1.69409931513988E-14));
#16417=DIRECTION('',(-0.707106781186585,4.09777199049619E-14,-0.70710678118651));
#16418=DIRECTION('',(0.,0.,-1.));
#16419=DIRECTION('',(-1.,0.,0.));
#16420=DIRECTION('',(0.,0.,-1.));
#16421=DIRECTION('',(-1.,0.,0.));
#16422=DIRECTION('',(0.,0.,1.));
#16423=DIRECTION('',(0.,1.,0.));
#16424=DIRECTION('',(0.,0.,1.));
#16425=DIRECTION('',(3.20622841942719E-14,-1.,-2.6903450842113E-14));
#16426=DIRECTION('',(0.173648177666964,2.73184799366429E-14,-0.984807753012202));
#16427=DIRECTION('',(0.984807753012211,1.05615708143971E-14,0.173648177666915));
#16428=DIRECTION('',(0.,1.,0.));
#16429=DIRECTION('',(-1.,0.,0.));
#16430=DIRECTION('',(0.,0.,-1.));
#16431=DIRECTION('',(0.,0.,-1.));
#16432=DIRECTION('',(-1.,0.,0.));
#16433=DIRECTION('',(0.,0.,1.));
#16434=DIRECTION('',(0.,0.,-1.));
#16435=DIRECTION('',(-1.,0.,0.));
#16436=DIRECTION('',(0.,0.,1.));
#16437=DIRECTION('',(1.,0.,0.));
#16438=DIRECTION('',(0.,1.,0.));
#16439=DIRECTION('',(0.,0.,1.));
#16440=DIRECTION('',(-1.,2.41270005758632E-13,0.));
#16441=DIRECTION('',(0.,0.,1.));
#16442=DIRECTION('',(0.,1.,0.));
#16443=DIRECTION('',(0.,0.,1.));
#16444=DIRECTION('',(0.,0.,1.));
#16445=DIRECTION('',(1.,-2.41270005758632E-13,0.));
#16446=DIRECTION('',(0.984807753012211,1.05615708143972E-14,-0.173648177666916));
#16447=DIRECTION('',(-3.20622841942655E-14,-1.,-2.69034508421121E-14));
#16448=DIRECTION('',(-1.,2.73184799366474E-14,0.));
#16449=DIRECTION('',(0.0157590095386061,0.0588134242587623,0.998144596110865));
#16450=DIRECTION('',(-0.89391175202766,0.448074518359429,-0.012288432927183));
#16451=DIRECTION('',(0.,0.,-1.));
#16452=DIRECTION('',(-1.,0.,0.));
#16453=DIRECTION('',(0.,0.,1.));
#16454=DIRECTION('',(1.,0.,0.));
#16455=DIRECTION('',(0.,0.,1.));
#16456=DIRECTION('',(1.,0.,0.));
#16457=DIRECTION('',(0.,0.,-1.));
#16458=DIRECTION('',(-1.,0.,0.));
#16459=DIRECTION('',(0.,0.,1.));
#16460=DIRECTION('',(1.,0.,0.));
#16461=DIRECTION('',(0.,0.,1.));
#16462=DIRECTION('',(1.,0.,0.));
#16463=DIRECTION('',(0.,0.,1.));
#16464=DIRECTION('',(1.,0.,0.));
#16465=DIRECTION('',(0.,0.,1.));
#16466=DIRECTION('',(1.,0.,0.));
#16467=DIRECTION('',(0.,0.,-1.));
#16468=DIRECTION('',(1.,0.,0.));
#16469=DIRECTION('',(0.,0.,-1.));
#16470=DIRECTION('',(1.,0.,0.));
#16471=DIRECTION('',(0.,0.,1.));
#16472=DIRECTION('',(1.,0.,0.));
#16473=DIRECTION('',(0.,0.,-1.));
#16474=DIRECTION('',(-1.,0.,0.));
#16475=DIRECTION('',(0.,0.,-1.));
#16476=DIRECTION('',(-1.,0.,0.));
#16477=DIRECTION('',(0.,0.,-1.));
#16478=DIRECTION('',(-1.,0.,0.));
#16479=DIRECTION('',(0.,0.,-1.));
#16480=DIRECTION('',(-1.,0.,0.));
#16481=DIRECTION('',(0.,0.,1.));
#16482=DIRECTION('',(1.,0.,0.));
#16483=DIRECTION('',(0.,0.,-1.));
#16484=DIRECTION('',(-1.,0.,0.));
#16485=DIRECTION('',(0.,0.,-1.));
#16486=DIRECTION('',(-1.,0.,0.));
#16487=DIRECTION('',(0.,0.,-1.));
#16488=DIRECTION('',(-1.,0.,0.));
#19109=CARTESIAN_POINT('',(0.,0.,0.));
#31722=CARTESIAN_POINT('',(-0.008264,0.0303108891324553,0.083));
#31723=CARTESIAN_POINT('',(-0.00826400000000004,0.0327856678737492,0.0831322916666668));
#31724=CARTESIAN_POINT('',(-0.00950138937064697,0.0349288891324553,0.0832645833333334));
#31725=CARTESIAN_POINT('',(-0.0107387787412939,0.0370721103911615,0.0833968750000001));
#31726=CARTESIAN_POINT('',(-0.012882,0.0383094997618084,0.0835291666666667));
#31727=CARTESIAN_POINT('',(-0.0150252212587062,0.0395468891324554,0.0836614583333334));
#31728=CARTESIAN_POINT('',(-0.0175,0.0395468891324554,0.08379375));
#31729=CARTESIAN_POINT('',(-0.0199747787412939,0.0395468891324554,0.0839260416666667));
#31730=CARTESIAN_POINT('',(-0.022118,0.0383094997618084,0.0840583333333334));
#31731=CARTESIAN_POINT('',(-0.0242612212587062,0.0370721103911615,0.084190625));
#31732=CARTESIAN_POINT('',(-0.0254986106293531,0.0349288891324553,0.0843229166666667));
#31733=CARTESIAN_POINT('',(-0.0267360000000001,0.0327856678737492,0.0844552083333334));
#31734=CARTESIAN_POINT('',(-0.026736,0.0303108891324553,0.0845875));
#31735=CARTESIAN_POINT('',(-0.0267360000000001,0.0278361103911615,0.0847197916666667));
#31736=CARTESIAN_POINT('',(-0.0254986106293531,0.0256928891324554,0.0848520833333334));
#31737=CARTESIAN_POINT('',(-0.0242612212587062,0.0235496678737492,0.0849843750000001));
#31738=CARTESIAN_POINT('',(-0.022118,0.0223122785031023,0.0851166666666667));
#31739=CARTESIAN_POINT('',(-0.0199747787412939,0.0210748891324554,0.0852489583333334));
#31740=CARTESIAN_POINT('',(-0.0175,0.0210748891324553,0.08538125));
#31741=CARTESIAN_POINT('',(-0.0150252212587062,0.0210748891324553,0.0855135416666667));
#31742=CARTESIAN_POINT('',(-0.012882,0.0223122785031023,0.0856458333333334));
#31743=CARTESIAN_POINT('',(-0.0107387787412939,0.0235496678737492,0.0857781250000001));
#31744=CARTESIAN_POINT('',(-0.00950138937064697,0.0256928891324554,0.0859104166666667));
#31745=CARTESIAN_POINT('',(-0.00826400000000005,0.0278361103911615,0.0860427083333334));
#31746=CARTESIAN_POINT('',(-0.008264,0.0303108891324553,0.086175));
#31747=CARTESIAN_POINT('',(-0.00826400000000004,0.0327856678737492,0.0863072916666667));
#31748=CARTESIAN_POINT('',(-0.00950138937064697,0.0349288891324553,0.0864395833333334));
#31749=CARTESIAN_POINT('',(-0.0107387787412939,0.0370721103911615,0.086571875));
#31750=CARTESIAN_POINT('',(-0.012882,0.0383094997618084,0.0867041666666667));
#31751=CARTESIAN_POINT('',(-0.0150252212587062,0.0395468891324554,0.0868364583333334));
#31752=CARTESIAN_POINT('',(-0.0175,0.0395468891324554,0.08696875));
#31753=CARTESIAN_POINT('',(-0.0199747787412939,0.0395468891324554,0.0871010416666667));
#31754=CARTESIAN_POINT('',(-0.022118,0.0383094997618084,0.0872333333333334));
#31755=CARTESIAN_POINT('',(-0.0242612212587062,0.0370721103911615,0.087365625));
#31756=CARTESIAN_POINT('',(-0.0254986106293531,0.0349288891324553,0.0874979166666667));
#31757=CARTESIAN_POINT('',(-0.0267360000000001,0.0327856678737492,0.0876302083333334));
#31758=CARTESIAN_POINT('',(-0.026736,0.0303108891324553,0.0877625));
#31759=CARTESIAN_POINT('',(-0.0267360000000001,0.0278361103911615,0.0878947916666667));
#31760=CARTESIAN_POINT('',(-0.0254986106293531,0.0256928891324554,0.0880270833333334));
#31761=CARTESIAN_POINT('',(-0.0242612212587062,0.0235496678737492,0.088159375));
#31762=CARTESIAN_POINT('',(-0.022118,0.0223122785031023,0.0882916666666667));
#31763=CARTESIAN_POINT('',(-0.0199747787412939,0.0210748891324554,0.0884239583333334));
#31764=CARTESIAN_POINT('',(-0.0175,0.0210748891324553,0.08855625));
#31765=CARTESIAN_POINT('',(-0.0150252212587062,0.0210748891324553,0.0886885416666667));
#31766=CARTESIAN_POINT('',(-0.012882,0.0223122785031023,0.0888208333333334));
#31767=CARTESIAN_POINT('',(-0.0107387787412939,0.0235496678737492,0.088953125));
#31768=CARTESIAN_POINT('',(-0.00950138937064697,0.0256928891324554,0.0890854166666667));
#31769=CARTESIAN_POINT('',(-0.00826400000000005,0.0278361103911615,0.0892177083333334));
#31770=CARTESIAN_POINT('',(-0.008264,0.0303108891324553,0.08935));
#31771=CARTESIAN_POINT('',(-0.00826400000000004,0.0327856678737492,0.0894822916666667));
#31772=CARTESIAN_POINT('',(-0.00950138937064697,0.0349288891324553,0.0896145833333333));
#31773=CARTESIAN_POINT('',(-0.0107387787412939,0.0370721103911615,0.0897468750000001));
#31774=CARTESIAN_POINT('',(-0.012882,0.0383094997618084,0.0898791666666667));
#31775=CARTESIAN_POINT('',(-0.0150252212587062,0.0395468891324554,0.0900114583333334));
#31776=CARTESIAN_POINT('',(-0.0175,0.0395468891324554,0.09014375));
#31777=CARTESIAN_POINT('',(-0.0199747787412939,0.0395468891324554,0.0902760416666667));
#31778=CARTESIAN_POINT('',(-0.022118,0.0383094997618084,0.0904083333333334));
#31779=CARTESIAN_POINT('',(-0.0242612212587062,0.0370721103911615,0.0905406250000001));
#31780=CARTESIAN_POINT('',(-0.0254986106293531,0.0349288891324553,0.0906729166666667));
#31781=CARTESIAN_POINT('',(-0.0267360000000001,0.0327856678737492,0.0908052083333334));
#31782=CARTESIAN_POINT('',(-0.026736,0.0303108891324553,0.0909375));
#31783=CARTESIAN_POINT('',(-0.00826400000000005,0.0303108891324554,0.0832047959597733));
#31784=CARTESIAN_POINT('',(-0.00826400000000005,0.0327856678737492,0.08333708762644));
#31785=CARTESIAN_POINT('',(-0.00950138937064697,0.0349288891324553,0.0834693792931066));
#31786=CARTESIAN_POINT('',(-0.0107387787412939,0.0370721103911615,0.0836016709597733));
#31787=CARTESIAN_POINT('',(-0.0128820000000001,0.0383094997618084,0.08373396262644));
#31788=CARTESIAN_POINT('',(-0.0150252212587062,0.0395468891324554,0.0838662542931067));
#31789=CARTESIAN_POINT('',(-0.0175000000000001,0.0395468891324553,0.0839985459597733));
#31790=CARTESIAN_POINT('',(-0.0199747787412939,0.0395468891324554,0.08413083762644));
#31791=CARTESIAN_POINT('',(-0.022118,0.0383094997618084,0.0842631292931066));
#31792=CARTESIAN_POINT('',(-0.0242612212587062,0.0370721103911614,0.0843954209597733));
#31793=CARTESIAN_POINT('',(-0.0254986106293531,0.0349288891324553,0.08452771262644));
#31794=CARTESIAN_POINT('',(-0.026736,0.0327856678737492,0.0846600042931067));
#31795=CARTESIAN_POINT('',(-0.026736,0.0303108891324554,0.0847922959597733));
#31796=CARTESIAN_POINT('',(-0.026736,0.0278361103911615,0.08492458762644));
#31797=CARTESIAN_POINT('',(-0.0254986106293531,0.0256928891324553,0.0850568792931066));
#31798=CARTESIAN_POINT('',(-0.0242612212587062,0.0235496678737492,0.0851891709597732));
#31799=CARTESIAN_POINT('',(-0.022118,0.0223122785031022,0.08532146262644));
#31800=CARTESIAN_POINT('',(-0.0199747787412939,0.0210748891324554,0.0854537542931067));
#31801=CARTESIAN_POINT('',(-0.0175000000000001,0.0210748891324553,0.0855860459597733));
#31802=CARTESIAN_POINT('',(-0.0150252212587062,0.0210748891324553,0.0857183376264399));
#31803=CARTESIAN_POINT('',(-0.0128820000000001,0.0223122785031022,0.0858506292931066));
#31804=CARTESIAN_POINT('',(-0.0107387787412939,0.0235496678737492,0.0859829209597734));
#31805=CARTESIAN_POINT('',(-0.00950138937064697,0.0256928891324553,0.08611521262644));
#31806=CARTESIAN_POINT('',(-0.00826400000000005,0.0278361103911615,0.0862475042931066));
#31807=CARTESIAN_POINT('',(-0.00826400000000005,0.0303108891324554,0.0863797959597733));
#31808=CARTESIAN_POINT('',(-0.00826400000000005,0.0327856678737492,0.08651208762644));
#31809=CARTESIAN_POINT('',(-0.00950138937064697,0.0349288891324553,0.0866443792931067));
#31810=CARTESIAN_POINT('',(-0.0107387787412939,0.0370721103911615,0.0867766709597732));
#31811=CARTESIAN_POINT('',(-0.0128820000000001,0.0383094997618084,0.08690896262644));
#31812=CARTESIAN_POINT('',(-0.0150252212587062,0.0395468891324554,0.0870412542931066));
#31813=CARTESIAN_POINT('',(-0.0175000000000001,0.0395468891324553,0.0871735459597733));
#31814=CARTESIAN_POINT('',(-0.0199747787412939,0.0395468891324554,0.08730583762644));
#31815=CARTESIAN_POINT('',(-0.022118,0.0383094997618084,0.0874381292931067));
#31816=CARTESIAN_POINT('',(-0.0242612212587062,0.0370721103911614,0.0875704209597733));
#31817=CARTESIAN_POINT('',(-0.0254986106293531,0.0349288891324553,0.08770271262644));
#31818=CARTESIAN_POINT('',(-0.026736,0.0327856678737492,0.0878350042931066));
#31819=CARTESIAN_POINT('',(-0.026736,0.0303108891324554,0.0879672959597733));
#31820=CARTESIAN_POINT('',(-0.026736,0.0278361103911615,0.0880995876264399));
#31821=CARTESIAN_POINT('',(-0.0254986106293531,0.0256928891324553,0.0882318792931067));
#31822=CARTESIAN_POINT('',(-0.0242612212587062,0.0235496678737492,0.0883641709597733));
#31823=CARTESIAN_POINT('',(-0.022118,0.0223122785031022,0.08849646262644));
#31824=CARTESIAN_POINT('',(-0.0199747787412939,0.0210748891324554,0.0886287542931066));
#31825=CARTESIAN_POINT('',(-0.0175000000000001,0.0210748891324553,0.0887610459597734));
#31826=CARTESIAN_POINT('',(-0.0150252212587062,0.0210748891324553,0.08889333762644));
#31827=CARTESIAN_POINT('',(-0.0128820000000001,0.0223122785031022,0.0890256292931067));
#31828=CARTESIAN_POINT('',(-0.0107387787412939,0.0235496678737492,0.0891579209597733));
#31829=CARTESIAN_POINT('',(-0.00950138937064697,0.0256928891324553,0.0892902126264399));
#31830=CARTESIAN_POINT('',(-0.00826400000000005,0.0278361103911615,0.0894225042931066));
#31831=CARTESIAN_POINT('',(-0.00826400000000005,0.0303108891324554,0.0895547959597733));
#31832=CARTESIAN_POINT('',(-0.00826400000000005,0.0327856678737492,0.08968708762644));
#31833=CARTESIAN_POINT('',(-0.00950138937064697,0.0349288891324553,0.0898193792931067));
#31834=CARTESIAN_POINT('',(-0.0107387787412939,0.0370721103911615,0.0899516709597733));
#31835=CARTESIAN_POINT('',(-0.0128820000000001,0.0383094997618084,0.09008396262644));
#31836=CARTESIAN_POINT('',(-0.0150252212587062,0.0395468891324554,0.0902162542931066));
#31837=CARTESIAN_POINT('',(-0.0175000000000001,0.0395468891324553,0.0903485459597733));
#31838=CARTESIAN_POINT('',(-0.0199747787412939,0.0395468891324554,0.09048083762644));
#31839=CARTESIAN_POINT('',(-0.022118,0.0383094997618084,0.0906131292931066));
#31840=CARTESIAN_POINT('',(-0.0242612212587062,0.0370721103911614,0.0907454209597733));
#31841=CARTESIAN_POINT('',(-0.0254986106293531,0.0349288891324553,0.0908777126264399));
#31842=CARTESIAN_POINT('',(-0.026736,0.0327856678737492,0.0910100042931066));
#31843=CARTESIAN_POINT('',(-0.026736,0.0303108891324554,0.0911422959597733));
#31844=CARTESIAN_POINT('',(-0.00834237202082059,0.0303108891324554,0.0833940027553488));
#31845=CARTESIAN_POINT('',(-0.00834237202082058,0.0327646681540611,0.0835262944220155));
#31846=CARTESIAN_POINT('',(-0.00956926153162349,0.0348897031220451,0.0836585860886822));
#31847=CARTESIAN_POINT('',(-0.0107961510424264,0.037014738090029,0.0837908777553489));
#31848=CARTESIAN_POINT('',(-0.0129211860104103,0.0382416276008319,0.0839231694220155));
#31849=CARTESIAN_POINT('',(-0.0150462209783942,0.0394685171116348,0.0840554610886822));
#31850=CARTESIAN_POINT('',(-0.0175000000000001,0.0394685171116348,0.0841877527553489));
#31851=CARTESIAN_POINT('',(-0.0199537790216058,0.0394685171116348,0.0843200444220155));
#31852=CARTESIAN_POINT('',(-0.0220788139895898,0.0382416276008319,0.0844523360886822));
#31853=CARTESIAN_POINT('',(-0.0242038489575737,0.037014738090029,0.0845846277553489));
#31854=CARTESIAN_POINT('',(-0.0254307384683766,0.0348897031220451,0.0847169194220155));
#31855=CARTESIAN_POINT('',(-0.0266576279791795,0.0327646681540611,0.0848492110886822));
#31856=CARTESIAN_POINT('',(-0.0266576279791795,0.0303108891324554,0.0849815027553489));
#31857=CARTESIAN_POINT('',(-0.0266576279791795,0.0278571101108495,0.0851137944220155));
#31858=CARTESIAN_POINT('',(-0.0254307384683766,0.0257320751428656,0.0852460860886822));
#31859=CARTESIAN_POINT('',(-0.0242038489575737,0.0236070401748817,0.0853783777553489));
#31860=CARTESIAN_POINT('',(-0.0220788139895898,0.0223801506640788,0.0855106694220155));
#31861=CARTESIAN_POINT('',(-0.0199537790216058,0.0211532611532759,0.0856429610886822));
#31862=CARTESIAN_POINT('',(-0.0175000000000001,0.0211532611532759,0.0857752527553489));
#31863=CARTESIAN_POINT('',(-0.0150462209783943,0.0211532611532759,0.0859075444220155));
#31864=CARTESIAN_POINT('',(-0.0129211860104103,0.0223801506640788,0.0860398360886822));
#31865=CARTESIAN_POINT('',(-0.0107961510424264,0.0236070401748817,0.0861721277553489));
#31866=CARTESIAN_POINT('',(-0.00956926153162349,0.0257320751428656,0.0863044194220156));
#31867=CARTESIAN_POINT('',(-0.00834237202082059,0.0278571101108495,0.0864367110886822));
#31868=CARTESIAN_POINT('',(-0.00834237202082059,0.0303108891324554,0.0865690027553489));
#31869=CARTESIAN_POINT('',(-0.00834237202082058,0.0327646681540611,0.0867012944220156));
#31870=CARTESIAN_POINT('',(-0.00956926153162349,0.0348897031220451,0.0868335860886822));
#31871=CARTESIAN_POINT('',(-0.0107961510424264,0.037014738090029,0.0869658777553489));
#31872=CARTESIAN_POINT('',(-0.0129211860104103,0.0382416276008319,0.0870981694220156));
#31873=CARTESIAN_POINT('',(-0.0150462209783942,0.0394685171116348,0.0872304610886822));
#31874=CARTESIAN_POINT('',(-0.0175000000000001,0.0394685171116348,0.0873627527553488));
#31875=CARTESIAN_POINT('',(-0.0199537790216058,0.0394685171116348,0.0874950444220156));
#31876=CARTESIAN_POINT('',(-0.0220788139895898,0.0382416276008319,0.0876273360886822));
#31877=CARTESIAN_POINT('',(-0.0242038489575737,0.037014738090029,0.0877596277553488));
#31878=CARTESIAN_POINT('',(-0.0254307384683766,0.0348897031220451,0.0878919194220156));
#31879=CARTESIAN_POINT('',(-0.0266576279791795,0.0327646681540611,0.0880242110886821));
#31880=CARTESIAN_POINT('',(-0.0266576279791795,0.0303108891324554,0.0881565027553489));
#31881=CARTESIAN_POINT('',(-0.0266576279791795,0.0278571101108495,0.0882887944220156));
#31882=CARTESIAN_POINT('',(-0.0254307384683766,0.0257320751428656,0.0884210860886821));
#31883=CARTESIAN_POINT('',(-0.0242038489575737,0.0236070401748817,0.0885533777553488));
#31884=CARTESIAN_POINT('',(-0.0220788139895898,0.0223801506640788,0.0886856694220155));
#31885=CARTESIAN_POINT('',(-0.0199537790216058,0.0211532611532759,0.0888179610886821));
#31886=CARTESIAN_POINT('',(-0.0175000000000001,0.0211532611532759,0.0889502527553488));
#31887=CARTESIAN_POINT('',(-0.0150462209783943,0.0211532611532759,0.0890825444220155));
#31888=CARTESIAN_POINT('',(-0.0129211860104103,0.0223801506640788,0.0892148360886822));
#31889=CARTESIAN_POINT('',(-0.0107961510424264,0.0236070401748817,0.0893471277553488));
#31890=CARTESIAN_POINT('',(-0.00956926153162349,0.0257320751428656,0.0894794194220155));
#31891=CARTESIAN_POINT('',(-0.00834237202082059,0.0278571101108495,0.0896117110886821));
#31892=CARTESIAN_POINT('',(-0.00834237202082059,0.0303108891324554,0.0897440027553488));
#31893=CARTESIAN_POINT('',(-0.00834237202082058,0.0327646681540611,0.0898762944220156));
#31894=CARTESIAN_POINT('',(-0.00956926153162349,0.0348897031220451,0.0900085860886822));
#31895=CARTESIAN_POINT('',(-0.0107961510424264,0.037014738090029,0.0901408777553488));
#31896=CARTESIAN_POINT('',(-0.0129211860104103,0.0382416276008319,0.0902731694220155));
#31897=CARTESIAN_POINT('',(-0.0150462209783942,0.0394685171116348,0.0904054610886822));
#31898=CARTESIAN_POINT('',(-0.0175000000000001,0.0394685171116348,0.0905377527553489));
#31899=CARTESIAN_POINT('',(-0.0199537790216058,0.0394685171116348,0.0906700444220155));
#31900=CARTESIAN_POINT('',(-0.0220788139895898,0.0382416276008319,0.0908023360886822));
#31901=CARTESIAN_POINT('',(-0.0242038489575737,0.037014738090029,0.0909346277553488));
#31902=CARTESIAN_POINT('',(-0.0254307384683766,0.0348897031220451,0.0910669194220155));
#31903=CARTESIAN_POINT('',(-0.0266576279791795,0.0327646681540611,0.0911992110886822));
#31904=CARTESIAN_POINT('',(-0.0266576279791795,0.0303108891324554,0.0913315027553488));
#31905=CARTESIAN_POINT('',(-0.0084871846327359,0.0303108891324553,0.0835388153672642));
#31906=CARTESIAN_POINT('',(-0.0084871846327359,0.0327258657316446,0.0836711070339308));
#31907=CARTESIAN_POINT('',(-0.00969467293233051,0.0348172968160874,0.0838033987005975));
#31908=CARTESIAN_POINT('',(-0.0109021612319251,0.0369087279005302,0.0839356903672642));
#31909=CARTESIAN_POINT('',(-0.012993592316368,0.0381162162001248,0.0840679820339308));
#31910=CARTESIAN_POINT('',(-0.0150850234008108,0.0393237044997195,0.0842002737005975));
#31911=CARTESIAN_POINT('',(-0.0175,0.0393237044997195,0.0843325653672642));
#31912=CARTESIAN_POINT('',(-0.0199149765991893,0.0393237044997195,0.0844648570339309));
#31913=CARTESIAN_POINT('',(-0.0220064076836321,0.0381162162001248,0.0845971487005975));
#31914=CARTESIAN_POINT('',(-0.024097838768075,0.0369087279005303,0.0847294403672642));
#31915=CARTESIAN_POINT('',(-0.0253053270676696,0.0348172968160874,0.0848617320339308));
#31916=CARTESIAN_POINT('',(-0.0265128153672642,0.0327258657316446,0.0849940237005975));
#31917=CARTESIAN_POINT('',(-0.0265128153672642,0.0303108891324553,0.0851263153672642));
#31918=CARTESIAN_POINT('',(-0.0265128153672642,0.0278959125332661,0.0852586070339309));
#31919=CARTESIAN_POINT('',(-0.0253053270676696,0.0258044814488233,0.0853908987005975));
#31920=CARTESIAN_POINT('',(-0.024097838768075,0.0237130503643804,0.0855231903672642));
#31921=CARTESIAN_POINT('',(-0.0220064076836321,0.0225055620647858,0.0856554820339308));
#31922=CARTESIAN_POINT('',(-0.0199149765991893,0.0212980737651912,0.0857877737005975));
#31923=CARTESIAN_POINT('',(-0.0175,0.0212980737651912,0.0859200653672642));
#31924=CARTESIAN_POINT('',(-0.0150850234008108,0.0212980737651912,0.0860523570339309));
#31925=CARTESIAN_POINT('',(-0.012993592316368,0.0225055620647858,0.0861846487005975));
#31926=CARTESIAN_POINT('',(-0.0109021612319251,0.0237130503643804,0.0863169403672642));
#31927=CARTESIAN_POINT('',(-0.00969467293233052,0.0258044814488233,0.0864492320339308));
#31928=CARTESIAN_POINT('',(-0.0084871846327359,0.0278959125332661,0.0865815237005975));
#31929=CARTESIAN_POINT('',(-0.0084871846327359,0.0303108891324553,0.0867138153672642));
#31930=CARTESIAN_POINT('',(-0.0084871846327359,0.0327258657316446,0.0868461070339309));
#31931=CARTESIAN_POINT('',(-0.00969467293233051,0.0348172968160874,0.0869783987005975));
#31932=CARTESIAN_POINT('',(-0.0109021612319251,0.0369087279005302,0.0871106903672642));
#31933=CARTESIAN_POINT('',(-0.012993592316368,0.0381162162001248,0.0872429820339308));
#31934=CARTESIAN_POINT('',(-0.0150850234008108,0.0393237044997195,0.0873752737005975));
#31935=CARTESIAN_POINT('',(-0.0175,0.0393237044997195,0.0875075653672642));
#31936=CARTESIAN_POINT('',(-0.0199149765991893,0.0393237044997195,0.0876398570339308));
#31937=CARTESIAN_POINT('',(-0.0220064076836321,0.0381162162001248,0.0877721487005975));
#31938=CARTESIAN_POINT('',(-0.024097838768075,0.0369087279005303,0.0879044403672642));
#31939=CARTESIAN_POINT('',(-0.0253053270676696,0.0348172968160874,0.0880367320339308));
#31940=CARTESIAN_POINT('',(-0.0265128153672642,0.0327258657316446,0.0881690237005976));
#31941=CARTESIAN_POINT('',(-0.0265128153672642,0.0303108891324553,0.0883013153672642));
#31942=CARTESIAN_POINT('',(-0.0265128153672642,0.0278959125332661,0.0884336070339309));
#31943=CARTESIAN_POINT('',(-0.0253053270676696,0.0258044814488233,0.0885658987005975));
#31944=CARTESIAN_POINT('',(-0.024097838768075,0.0237130503643804,0.0886981903672642));
#31945=CARTESIAN_POINT('',(-0.0220064076836321,0.0225055620647858,0.0888304820339308));
#31946=CARTESIAN_POINT('',(-0.0199149765991893,0.0212980737651912,0.0889627737005975));
#31947=CARTESIAN_POINT('',(-0.0175,0.0212980737651912,0.0890950653672642));
#31948=CARTESIAN_POINT('',(-0.0150850234008108,0.0212980737651912,0.0892273570339309));
#31949=CARTESIAN_POINT('',(-0.012993592316368,0.0225055620647858,0.0893596487005975));
#31950=CARTESIAN_POINT('',(-0.0109021612319251,0.0237130503643804,0.0894919403672642));
#31951=CARTESIAN_POINT('',(-0.00969467293233052,0.0258044814488233,0.0896242320339308));
#31952=CARTESIAN_POINT('',(-0.0084871846327359,0.0278959125332661,0.0897565237005975));
#31953=CARTESIAN_POINT('',(-0.0084871846327359,0.0303108891324553,0.0898888153672642));
#31954=CARTESIAN_POINT('',(-0.0084871846327359,0.0327258657316446,0.0900211070339309));
#31955=CARTESIAN_POINT('',(-0.00969467293233051,0.0348172968160874,0.0901533987005975));
#31956=CARTESIAN_POINT('',(-0.0109021612319251,0.0369087279005302,0.0902856903672642));
#31957=CARTESIAN_POINT('',(-0.012993592316368,0.0381162162001248,0.0904179820339308));
#31958=CARTESIAN_POINT('',(-0.0150850234008108,0.0393237044997195,0.0905502737005975));
#31959=CARTESIAN_POINT('',(-0.0175,0.0393237044997195,0.0906825653672642));
#31960=CARTESIAN_POINT('',(-0.0199149765991893,0.0393237044997195,0.0908148570339309));
#31961=CARTESIAN_POINT('',(-0.0220064076836321,0.0381162162001248,0.0909471487005975));
#31962=CARTESIAN_POINT('',(-0.024097838768075,0.0369087279005303,0.0910794403672642));
#31963=CARTESIAN_POINT('',(-0.0253053270676696,0.0348172968160874,0.0912117320339308));
#31964=CARTESIAN_POINT('',(-0.0265128153672642,0.0327258657316446,0.0913440237005975));
#31965=CARTESIAN_POINT('',(-0.0265128153672642,0.0303108891324553,0.0914763153672642));
#31966=CARTESIAN_POINT('',(-0.009026,0.0303108891324553,0.083));
#31967=CARTESIAN_POINT('',(-0.008264,0.0303108891324553,0.083));
#31968=CARTESIAN_POINT('',(-0.0084871846327359,0.0303108891324553,0.0835388153672642));
#31969=CARTESIAN_POINT('',(-0.0084871846327359,0.0303108891324553,0.0835388153672642));
#31970=CARTESIAN_POINT('',(-0.0084871846327359,0.0327258657316446,0.0836711070339308));
#31971=CARTESIAN_POINT('',(-0.00969467293233051,0.0348172968160874,0.0838033987005975));
#31972=CARTESIAN_POINT('',(-0.0109021612319251,0.0369087279005302,0.0839356903672642));
#31973=CARTESIAN_POINT('',(-0.012993592316368,0.0381162162001248,0.0840679820339308));
#31974=CARTESIAN_POINT('',(-0.0150850234008108,0.0393237044997195,0.0842002737005975));
#31975=CARTESIAN_POINT('',(-0.0175,0.0393237044997195,0.0843325653672642));
#31976=CARTESIAN_POINT('',(-0.0199149765991893,0.0393237044997195,0.0844648570339309));
#31977=CARTESIAN_POINT('',(-0.0220064076836321,0.0381162162001248,0.0845971487005975));
#31978=CARTESIAN_POINT('',(-0.024097838768075,0.0369087279005303,0.0847294403672642));
#31979=CARTESIAN_POINT('',(-0.0253053270676696,0.0348172968160874,0.0848617320339308));
#31980=CARTESIAN_POINT('',(-0.0265128153672642,0.0327258657316446,0.0849940237005975));
#31981=CARTESIAN_POINT('',(-0.0265128153672642,0.0303108891324553,0.0851263153672642));
#31982=CARTESIAN_POINT('',(-0.0265128153672642,0.0278959125332661,0.0852586070339309));
#31983=CARTESIAN_POINT('',(-0.0253053270676696,0.0258044814488233,0.0853908987005975));
#31984=CARTESIAN_POINT('',(-0.024097838768075,0.0237130503643804,0.0855231903672642));
#31985=CARTESIAN_POINT('',(-0.0220064076836321,0.0225055620647858,0.0856554820339308));
#31986=CARTESIAN_POINT('',(-0.0199149765991893,0.0212980737651912,0.0857877737005975));
#31987=CARTESIAN_POINT('',(-0.0175,0.0212980737651912,0.0859200653672642));
#31988=CARTESIAN_POINT('',(-0.0150850234008108,0.0212980737651912,0.0860523570339309));
#31989=CARTESIAN_POINT('',(-0.012993592316368,0.0225055620647858,0.0861846487005975));
#31990=CARTESIAN_POINT('',(-0.0109021612319251,0.0237130503643804,0.0863169403672642));
#31991=CARTESIAN_POINT('',(-0.00969467293233052,0.0258044814488233,0.0864492320339308));
#31992=CARTESIAN_POINT('',(-0.00848718463273591,0.0278959125332661,0.0865815237005975));
#31993=CARTESIAN_POINT('',(-0.0084871846327359,0.0303108891324553,0.0867138153672642));
#31994=CARTESIAN_POINT('',(-0.0084871846327359,0.0327258657316446,0.0868461070339309));
#31995=CARTESIAN_POINT('',(-0.00969467293233051,0.0348172968160874,0.0869783987005975));
#31996=CARTESIAN_POINT('',(-0.0109021612319251,0.0369087279005302,0.0871106903672642));
#31997=CARTESIAN_POINT('',(-0.012993592316368,0.0381162162001248,0.0872429820339308));
#31998=CARTESIAN_POINT('',(-0.0150850234008108,0.0393237044997195,0.0873752737005975));
#31999=CARTESIAN_POINT('',(-0.0175,0.0393237044997195,0.0875075653672642));
#32000=CARTESIAN_POINT('',(-0.0199149765991893,0.0393237044997195,0.0876398570339309));
#32001=CARTESIAN_POINT('',(-0.0220064076836321,0.0381162162001248,0.0877721487005975));
#32002=CARTESIAN_POINT('',(-0.024097838768075,0.0369087279005303,0.0879044403672641));
#32003=CARTESIAN_POINT('',(-0.0253053270676696,0.0348172968160874,0.0880367320339308));
#32004=CARTESIAN_POINT('',(-0.0265128153672642,0.0327258657316446,0.0881690237005976));
#32005=CARTESIAN_POINT('',(-0.0265128153672642,0.0303108891324553,0.0883013153672642));
#32006=CARTESIAN_POINT('',(-0.0265128153672642,0.0278959125332661,0.0884336070339309));
#32007=CARTESIAN_POINT('',(-0.0253053270676696,0.0258044814488233,0.0885658987005975));
#32008=CARTESIAN_POINT('',(-0.024097838768075,0.0237130503643804,0.0886981903672642));
#32009=CARTESIAN_POINT('',(-0.0220064076836321,0.0225055620647858,0.0888304820339308));
#32010=CARTESIAN_POINT('',(-0.0199149765991893,0.0212980737651912,0.0889627737005975));
#32011=CARTESIAN_POINT('',(-0.0175,0.0212980737651912,0.0890950653672642));
#32012=CARTESIAN_POINT('',(-0.0150850234008108,0.0212980737651912,0.0892273570339309));
#32013=CARTESIAN_POINT('',(-0.012993592316368,0.0225055620647858,0.0893596487005975));
#32014=CARTESIAN_POINT('',(-0.0109021612319251,0.0237130503643804,0.0894919403672642));
#32015=CARTESIAN_POINT('',(-0.00969467293233052,0.0258044814488233,0.0896242320339308));
#32016=CARTESIAN_POINT('',(-0.00848718463273591,0.0278959125332661,0.0897565237005975));
#32017=CARTESIAN_POINT('',(-0.0084871846327359,0.0303108891324553,0.0898888153672642));
#32018=CARTESIAN_POINT('',(-0.0084871846327359,0.0327258657316446,0.0900211070339309));
#32019=CARTESIAN_POINT('',(-0.00969467293233051,0.0348172968160874,0.0901533987005975));
#32020=CARTESIAN_POINT('',(-0.0109021612319251,0.0369087279005302,0.0902856903672642));
#32021=CARTESIAN_POINT('',(-0.012993592316368,0.0381162162001248,0.0904179820339308));
#32022=CARTESIAN_POINT('',(-0.0150850234008108,0.0393237044997195,0.0905502737005975));
#32023=CARTESIAN_POINT('',(-0.0175,0.0393237044997195,0.0906825653672642));
#32024=CARTESIAN_POINT('',(-0.0199149765991893,0.0393237044997195,0.0908148570339309));
#32025=CARTESIAN_POINT('',(-0.0220064076836321,0.0381162162001248,0.0909471487005975));
#32026=CARTESIAN_POINT('',(-0.024097838768075,0.0369087279005303,0.0910794403672642));
#32027=CARTESIAN_POINT('',(-0.0253053270676696,0.0348172968160874,0.0912117320339308));
#32028=CARTESIAN_POINT('',(-0.0265128153672642,0.0327258657316446,0.0913440237005975));
#32029=CARTESIAN_POINT('',(-0.0265128153672642,0.0303108891324553,0.0914763153672642));
#32030=CARTESIAN_POINT('',(-0.0265128153672642,0.0303108891324553,0.0914763153672642));
#32031=CARTESIAN_POINT('',(-0.025974,0.0303108891324553,0.0909375));
#32032=CARTESIAN_POINT('',(-0.026736,0.0303108891324553,0.0909375));
#32033=CARTESIAN_POINT('',(-0.008264,0.0303108891324553,0.08935));
#32034=CARTESIAN_POINT('',(-0.00826400000000002,0.0327856678737492,0.0894822916666667));
#32035=CARTESIAN_POINT('',(-0.00950138937064697,0.0349288891324553,0.0896145833333333));
#32036=CARTESIAN_POINT('',(-0.0107387787412939,0.0370721103911615,0.0897468750000001));
#32037=CARTESIAN_POINT('',(-0.012882,0.0383094997618084,0.0898791666666667));
#32038=CARTESIAN_POINT('',(-0.0150252212587062,0.0395468891324554,0.0900114583333334));
#32039=CARTESIAN_POINT('',(-0.0175,0.0395468891324554,0.09014375));
#32040=CARTESIAN_POINT('',(-0.0199747787412939,0.0395468891324554,0.0902760416666667));
#32041=CARTESIAN_POINT('',(-0.022118,0.0383094997618084,0.0904083333333334));
#32042=CARTESIAN_POINT('',(-0.0242612212587062,0.0370721103911615,0.0905406250000001));
#32043=CARTESIAN_POINT('',(-0.0254986106293531,0.0349288891324553,0.0906729166666667));
#32044=CARTESIAN_POINT('',(-0.0267360000000001,0.0327856678737492,0.0908052083333334));
#32045=CARTESIAN_POINT('',(-0.026736,0.0303108891324553,0.0909375));
#32046=CARTESIAN_POINT('',(-0.008264,0.0303108891324553,0.08935));
#32047=CARTESIAN_POINT('',(-0.026736,0.0303108891324553,0.0877625));
#32048=CARTESIAN_POINT('',(-0.0267360000000001,0.0278361103911614,0.0878947916666667));
#32049=CARTESIAN_POINT('',(-0.0254986106293531,0.0256928891324554,0.0880270833333334));
#32050=CARTESIAN_POINT('',(-0.0242612212587062,0.0235496678737492,0.088159375));
#32051=CARTESIAN_POINT('',(-0.022118,0.0223122785031023,0.0882916666666667));
#32052=CARTESIAN_POINT('',(-0.0199747787412939,0.0210748891324553,0.0884239583333334));
#32053=CARTESIAN_POINT('',(-0.0175,0.0210748891324553,0.08855625));
#32054=CARTESIAN_POINT('',(-0.0150252212587062,0.0210748891324553,0.0886885416666667));
#32055=CARTESIAN_POINT('',(-0.012882,0.0223122785031023,0.0888208333333334));
#32056=CARTESIAN_POINT('',(-0.0107387787412939,0.0235496678737492,0.088953125));
#32057=CARTESIAN_POINT('',(-0.00950138937064697,0.0256928891324554,0.0890854166666667));
#32058=CARTESIAN_POINT('',(-0.00826400000000006,0.0278361103911614,0.0892177083333334));
#32059=CARTESIAN_POINT('',(-0.008264,0.0303108891324553,0.08935));
#32060=CARTESIAN_POINT('',(-0.026736,0.0303108891324553,0.0877625));
#32061=CARTESIAN_POINT('',(-0.008264,0.0303108891324553,0.086175));
#32062=CARTESIAN_POINT('',(-0.00826400000000003,0.0327856678737492,0.0863072916666667));
#32063=CARTESIAN_POINT('',(-0.00950138937064697,0.0349288891324553,0.0864395833333334));
#32064=CARTESIAN_POINT('',(-0.0107387787412939,0.0370721103911615,0.086571875));
#32065=CARTESIAN_POINT('',(-0.012882,0.0383094997618084,0.0867041666666667));
#32066=CARTESIAN_POINT('',(-0.0150252212587062,0.0395468891324554,0.0868364583333334));
#32067=CARTESIAN_POINT('',(-0.0175,0.0395468891324554,0.08696875));
#32068=CARTESIAN_POINT('',(-0.0199747787412939,0.0395468891324554,0.0871010416666667));
#32069=CARTESIAN_POINT('',(-0.022118,0.0383094997618084,0.0872333333333334));
#32070=CARTESIAN_POINT('',(-0.0242612212587062,0.0370721103911615,0.087365625));
#32071=CARTESIAN_POINT('',(-0.0254986106293531,0.0349288891324553,0.0874979166666667));
#32072=CARTESIAN_POINT('',(-0.0267360000000001,0.0327856678737492,0.0876302083333333));
#32073=CARTESIAN_POINT('',(-0.026736,0.0303108891324553,0.0877625));
#32074=CARTESIAN_POINT('',(-0.008264,0.0303108891324553,0.086175));
#32075=CARTESIAN_POINT('',(-0.026736,0.0303108891324553,0.0845875));
#32076=CARTESIAN_POINT('',(-0.0267360000000001,0.0278361103911614,0.0847197916666667));
#32077=CARTESIAN_POINT('',(-0.0254986106293531,0.0256928891324554,0.0848520833333334));
#32078=CARTESIAN_POINT('',(-0.0242612212587062,0.0235496678737492,0.0849843750000001));
#32079=CARTESIAN_POINT('',(-0.022118,0.0223122785031023,0.0851166666666667));
#32080=CARTESIAN_POINT('',(-0.0199747787412939,0.0210748891324553,0.0852489583333334));
#32081=CARTESIAN_POINT('',(-0.0175,0.0210748891324553,0.08538125));
#32082=CARTESIAN_POINT('',(-0.0150252212587062,0.0210748891324553,0.0855135416666667));
#32083=CARTESIAN_POINT('',(-0.012882,0.0223122785031023,0.0856458333333334));
#32084=CARTESIAN_POINT('',(-0.0107387787412939,0.0235496678737492,0.0857781250000001));
#32085=CARTESIAN_POINT('',(-0.00950138937064697,0.0256928891324554,0.0859104166666667));
#32086=CARTESIAN_POINT('',(-0.00826400000000006,0.0278361103911614,0.0860427083333333));
#32087=CARTESIAN_POINT('',(-0.008264,0.0303108891324553,0.086175));
#32088=CARTESIAN_POINT('',(-0.026736,0.0303108891324553,0.0845875));
#32089=CARTESIAN_POINT('',(-0.008264,0.0303108891324553,0.083));
#32090=CARTESIAN_POINT('',(-0.00826400000000004,0.0327856678737492,0.0831322916666668));
#32091=CARTESIAN_POINT('',(-0.00950138937064697,0.0349288891324553,0.0832645833333334));
#32092=CARTESIAN_POINT('',(-0.0107387787412939,0.0370721103911615,0.0833968750000001));
#32093=CARTESIAN_POINT('',(-0.012882,0.0383094997618084,0.0835291666666667));
#32094=CARTESIAN_POINT('',(-0.0150252212587062,0.0395468891324554,0.0836614583333334));
#32095=CARTESIAN_POINT('',(-0.0175,0.0395468891324554,0.08379375));
#32096=CARTESIAN_POINT('',(-0.0199747787412939,0.0395468891324554,0.0839260416666667));
#32097=CARTESIAN_POINT('',(-0.022118,0.0383094997618084,0.0840583333333334));
#32098=CARTESIAN_POINT('',(-0.0242612212587062,0.0370721103911615,0.084190625));
#32099=CARTESIAN_POINT('',(-0.0254986106293531,0.0349288891324553,0.0843229166666667));
#32100=CARTESIAN_POINT('',(-0.0267360000000001,0.0327856678737491,0.0844552083333334));
#32101=CARTESIAN_POINT('',(-0.026736,0.0303108891324553,0.0845875));
#32102=CARTESIAN_POINT('',(-0.0084871846327359,0.0303108891324553,0.0835388153672642));
#32103=CARTESIAN_POINT('',(-0.0084871846327359,0.0327258657316446,0.0836711070339308));
#32104=CARTESIAN_POINT('',(-0.00969467293233052,0.0348172968160874,0.0838033987005975));
#32105=CARTESIAN_POINT('',(-0.0109021612319251,0.0369087279005302,0.0839356903672642));
#32106=CARTESIAN_POINT('',(-0.012993592316368,0.0381162162001248,0.0840679820339308));
#32107=CARTESIAN_POINT('',(-0.0150850234008108,0.0393237044997195,0.0842002737005975));
#32108=CARTESIAN_POINT('',(-0.0175,0.0393237044997195,0.0843325653672642));
#32109=CARTESIAN_POINT('',(-0.0199149765991893,0.0393237044997195,0.0844648570339309));
#32110=CARTESIAN_POINT('',(-0.0220064076836321,0.0381162162001248,0.0845971487005975));
#32111=CARTESIAN_POINT('',(-0.024097838768075,0.0369087279005302,0.0847294403672642));
#32112=CARTESIAN_POINT('',(-0.0253053270676696,0.0348172968160874,0.0848617320339308));
#32113=CARTESIAN_POINT('',(-0.0265128153672642,0.0327258657316446,0.0849940237005975));
#32114=CARTESIAN_POINT('',(-0.0265128153672642,0.0303108891324553,0.0851263153672642));
#32115=CARTESIAN_POINT('',(-0.0265128153672642,0.0278959125332661,0.0852586070339309));
#32116=CARTESIAN_POINT('',(-0.0253053270676696,0.0258044814488233,0.0853908987005975));
#32117=CARTESIAN_POINT('',(-0.024097838768075,0.0237130503643804,0.0855231903672642));
#32118=CARTESIAN_POINT('',(-0.0220064076836321,0.0225055620647858,0.0856554820339308));
#32119=CARTESIAN_POINT('',(-0.0199149765991893,0.0212980737651912,0.0857877737005975));
#32120=CARTESIAN_POINT('',(-0.0175,0.0212980737651912,0.0859200653672642));
#32121=CARTESIAN_POINT('',(-0.0150850234008108,0.0212980737651912,0.0860523570339309));
#32122=CARTESIAN_POINT('',(-0.012993592316368,0.0225055620647858,0.0861846487005975));
#32123=CARTESIAN_POINT('',(-0.0109021612319251,0.0237130503643804,0.0863169403672642));
#32124=CARTESIAN_POINT('',(-0.00969467293233052,0.0258044814488233,0.0864492320339308));
#32125=CARTESIAN_POINT('',(-0.0084871846327359,0.0278959125332661,0.0865815237005975));
#32126=CARTESIAN_POINT('',(-0.0084871846327359,0.0303108891324553,0.0867138153672642));
#32127=CARTESIAN_POINT('',(-0.0084871846327359,0.0327258657316446,0.0868461070339309));
#32128=CARTESIAN_POINT('',(-0.00969467293233052,0.0348172968160874,0.0869783987005975));
#32129=CARTESIAN_POINT('',(-0.0109021612319251,0.0369087279005302,0.0871106903672642));
#32130=CARTESIAN_POINT('',(-0.012993592316368,0.0381162162001248,0.0872429820339308));
#32131=CARTESIAN_POINT('',(-0.0150850234008108,0.0393237044997195,0.0873752737005975));
#32132=CARTESIAN_POINT('',(-0.0175,0.0393237044997195,0.0875075653672642));
#32133=CARTESIAN_POINT('',(-0.0199149765991893,0.0393237044997195,0.0876398570339308));
#32134=CARTESIAN_POINT('',(-0.0220064076836321,0.0381162162001248,0.0877721487005975));
#32135=CARTESIAN_POINT('',(-0.024097838768075,0.0369087279005302,0.0879044403672642));
#32136=CARTESIAN_POINT('',(-0.0253053270676696,0.0348172968160874,0.0880367320339308));
#32137=CARTESIAN_POINT('',(-0.0265128153672642,0.0327258657316446,0.0881690237005976));
#32138=CARTESIAN_POINT('',(-0.0265128153672642,0.0303108891324553,0.0883013153672642));
#32139=CARTESIAN_POINT('',(-0.0265128153672642,0.0278959125332661,0.0884336070339309));
#32140=CARTESIAN_POINT('',(-0.0253053270676696,0.0258044814488233,0.0885658987005975));
#32141=CARTESIAN_POINT('',(-0.024097838768075,0.0237130503643804,0.0886981903672642));
#32142=CARTESIAN_POINT('',(-0.0220064076836321,0.0225055620647858,0.0888304820339308));
#32143=CARTESIAN_POINT('',(-0.0199149765991893,0.0212980737651912,0.0889627737005975));
#32144=CARTESIAN_POINT('',(-0.0175,0.0212980737651912,0.0890950653672642));
#32145=CARTESIAN_POINT('',(-0.0150850234008108,0.0212980737651912,0.0892273570339309));
#32146=CARTESIAN_POINT('',(-0.012993592316368,0.0225055620647858,0.0893596487005975));
#32147=CARTESIAN_POINT('',(-0.0109021612319251,0.0237130503643804,0.0894919403672642));
#32148=CARTESIAN_POINT('',(-0.00969467293233052,0.0258044814488233,0.0896242320339308));
#32149=CARTESIAN_POINT('',(-0.0084871846327359,0.0278959125332661,0.0897565237005975));
#32150=CARTESIAN_POINT('',(-0.0084871846327359,0.0303108891324553,0.0898888153672642));
#32151=CARTESIAN_POINT('',(-0.0084871846327359,0.0327258657316446,0.0900211070339309));
#32152=CARTESIAN_POINT('',(-0.00969467293233052,0.0348172968160874,0.0901533987005975));
#32153=CARTESIAN_POINT('',(-0.0109021612319251,0.0369087279005302,0.0902856903672642));
#32154=CARTESIAN_POINT('',(-0.012993592316368,0.0381162162001248,0.0904179820339308));
#32155=CARTESIAN_POINT('',(-0.0150850234008108,0.0393237044997195,0.0905502737005975));
#32156=CARTESIAN_POINT('',(-0.0175,0.0393237044997195,0.0906825653672642));
#32157=CARTESIAN_POINT('',(-0.0199149765991893,0.0393237044997195,0.0908148570339309));
#32158=CARTESIAN_POINT('',(-0.0220064076836321,0.0381162162001248,0.0909471487005975));
#32159=CARTESIAN_POINT('',(-0.024097838768075,0.0369087279005302,0.0910794403672642));
#32160=CARTESIAN_POINT('',(-0.0253053270676696,0.0348172968160874,0.0912117320339308));
#32161=CARTESIAN_POINT('',(-0.0265128153672642,0.0327258657316446,0.0913440237005975));
#32162=CARTESIAN_POINT('',(-0.0265128153672642,0.0303108891324553,0.0914763153672642));
#32163=CARTESIAN_POINT('',(-0.00910761536726419,0.0303108891324553,0.0841592461017925));
#32164=CARTESIAN_POINT('',(-0.00910761536726418,0.0325596218173683,0.0842915377684592));
#32165=CARTESIAN_POINT('',(-0.0102319817097207,0.0345070814488233,0.0844238294351258));
#32166=CARTESIAN_POINT('',(-0.0113563480521771,0.0364545410802783,0.0845561211017925));
#32167=CARTESIAN_POINT('',(-0.0133038076836321,0.0375789074227347,0.0846884127684591));
#32168=CARTESIAN_POINT('',(-0.0152512673150871,0.0387032737651912,0.0848207044351258));
#32169=CARTESIAN_POINT('',(-0.0175,0.0387032737651912,0.0849529961017925));
#32170=CARTESIAN_POINT('',(-0.019748732684913,0.0387032737651912,0.0850852877684591));
#32171=CARTESIAN_POINT('',(-0.0216961923163679,0.0375789074227348,0.0852175794351258));
#32172=CARTESIAN_POINT('',(-0.023643651947823,0.0364545410802783,0.0853498711017925));
#32173=CARTESIAN_POINT('',(-0.0247680182902794,0.0345070814488233,0.0854821627684591));
#32174=CARTESIAN_POINT('',(-0.0258923846327359,0.0325596218173683,0.0856144544351258));
#32175=CARTESIAN_POINT('',(-0.0258923846327359,0.0303108891324553,0.0857467461017925));
#32176=CARTESIAN_POINT('',(-0.0258923846327359,0.0280621564475424,0.0858790377684592));
#32177=CARTESIAN_POINT('',(-0.0247680182902794,0.0261146968160874,0.0860113294351258));
#32178=CARTESIAN_POINT('',(-0.023643651947823,0.0241672371846324,0.0861436211017925));
#32179=CARTESIAN_POINT('',(-0.021696192316368,0.023042870842176,0.0862759127684591));
#32180=CARTESIAN_POINT('',(-0.019748732684913,0.0219185044997195,0.0864082044351258));
#32181=CARTESIAN_POINT('',(-0.0175,0.0219185044997195,0.0865404961017925));
#32182=CARTESIAN_POINT('',(-0.0152512673150871,0.0219185044997195,0.0866727877684591));
#32183=CARTESIAN_POINT('',(-0.0133038076836321,0.023042870842176,0.0868050794351258));
#32184=CARTESIAN_POINT('',(-0.0113563480521771,0.0241672371846324,0.0869373711017925));
#32185=CARTESIAN_POINT('',(-0.0102319817097207,0.0261146968160874,0.0870696627684591));
#32186=CARTESIAN_POINT('',(-0.00910761536726419,0.0280621564475424,0.0872019544351259));
#32187=CARTESIAN_POINT('',(-0.00910761536726419,0.0303108891324553,0.0873342461017925));
#32188=CARTESIAN_POINT('',(-0.00910761536726418,0.0325596218173683,0.0874665377684592));
#32189=CARTESIAN_POINT('',(-0.0102319817097207,0.0345070814488233,0.0875988294351258));
#32190=CARTESIAN_POINT('',(-0.0113563480521771,0.0364545410802783,0.0877311211017925));
#32191=CARTESIAN_POINT('',(-0.0133038076836321,0.0375789074227347,0.0878634127684591));
#32192=CARTESIAN_POINT('',(-0.0152512673150871,0.0387032737651912,0.0879957044351258));
#32193=CARTESIAN_POINT('',(-0.0175,0.0387032737651912,0.0881279961017925));
#32194=CARTESIAN_POINT('',(-0.019748732684913,0.0387032737651912,0.0882602877684591));
#32195=CARTESIAN_POINT('',(-0.0216961923163679,0.0375789074227348,0.0883925794351258));
#32196=CARTESIAN_POINT('',(-0.023643651947823,0.0364545410802783,0.0885248711017924));
#32197=CARTESIAN_POINT('',(-0.0247680182902794,0.0345070814488233,0.0886571627684591));
#32198=CARTESIAN_POINT('',(-0.0258923846327359,0.0325596218173683,0.0887894544351258));
#32199=CARTESIAN_POINT('',(-0.0258923846327359,0.0303108891324553,0.0889217461017925));
#32200=CARTESIAN_POINT('',(-0.0258923846327359,0.0280621564475424,0.0890540377684592));
#32201=CARTESIAN_POINT('',(-0.0247680182902794,0.0261146968160874,0.0891863294351258));
#32202=CARTESIAN_POINT('',(-0.023643651947823,0.0241672371846324,0.0893186211017925));
#32203=CARTESIAN_POINT('',(-0.021696192316368,0.023042870842176,0.0894509127684591));
#32204=CARTESIAN_POINT('',(-0.019748732684913,0.0219185044997195,0.0895832044351258));
#32205=CARTESIAN_POINT('',(-0.0175,0.0219185044997195,0.0897154961017925));
#32206=CARTESIAN_POINT('',(-0.0152512673150871,0.0219185044997195,0.0898477877684591));
#32207=CARTESIAN_POINT('',(-0.0133038076836321,0.023042870842176,0.0899800794351258));
#32208=CARTESIAN_POINT('',(-0.0113563480521771,0.0241672371846324,0.0901123711017924));
#32209=CARTESIAN_POINT('',(-0.0102319817097207,0.0261146968160874,0.0902446627684591));
#32210=CARTESIAN_POINT('',(-0.00910761536726419,0.0280621564475424,0.0903769544351259));
#32211=CARTESIAN_POINT('',(-0.00910761536726419,0.0303108891324553,0.0905092461017925));
#32212=CARTESIAN_POINT('',(-0.00910761536726418,0.0325596218173683,0.0906415377684592));
#32213=CARTESIAN_POINT('',(-0.0102319817097207,0.0345070814488233,0.0907738294351258));
#32214=CARTESIAN_POINT('',(-0.0113563480521771,0.0364545410802783,0.0909061211017925));
#32215=CARTESIAN_POINT('',(-0.0133038076836321,0.0375789074227347,0.0910384127684591));
#32216=CARTESIAN_POINT('',(-0.0152512673150871,0.0387032737651912,0.0911707044351258));
#32217=CARTESIAN_POINT('',(-0.0175,0.0387032737651912,0.0913029961017925));
#32218=CARTESIAN_POINT('',(-0.019748732684913,0.0387032737651912,0.0914352877684591));
#32219=CARTESIAN_POINT('',(-0.0216961923163679,0.0375789074227348,0.0915675794351258));
#32220=CARTESIAN_POINT('',(-0.023643651947823,0.0364545410802783,0.0916998711017924));
#32221=CARTESIAN_POINT('',(-0.0247680182902794,0.0345070814488233,0.0918321627684591));
#32222=CARTESIAN_POINT('',(-0.0258923846327359,0.0325596218173683,0.0919644544351259));
#32223=CARTESIAN_POINT('',(-0.0258923846327359,0.0303108891324553,0.0920967461017925));
#32224=CARTESIAN_POINT('',(-0.00910761536726419,0.0303108891324553,0.0841592461017925));
#32225=CARTESIAN_POINT('',(-0.00910761536726419,0.0325596218173683,0.0842915377684592));
#32226=CARTESIAN_POINT('',(-0.0102319817097207,0.0345070814488233,0.0844238294351258));
#32227=CARTESIAN_POINT('',(-0.0113563480521771,0.0364545410802783,0.0845561211017925));
#32228=CARTESIAN_POINT('',(-0.0133038076836321,0.0375789074227347,0.0846884127684591));
#32229=CARTESIAN_POINT('',(-0.0152512673150871,0.0387032737651912,0.0848207044351258));
#32230=CARTESIAN_POINT('',(-0.0175,0.0387032737651912,0.0849529961017925));
#32231=CARTESIAN_POINT('',(-0.019748732684913,0.0387032737651912,0.0850852877684591));
#32232=CARTESIAN_POINT('',(-0.0216961923163679,0.0375789074227348,0.0852175794351258));
#32233=CARTESIAN_POINT('',(-0.023643651947823,0.0364545410802783,0.0853498711017925));
#32234=CARTESIAN_POINT('',(-0.0247680182902794,0.0345070814488233,0.0854821627684591));
#32235=CARTESIAN_POINT('',(-0.0258923846327359,0.0325596218173683,0.0856144544351258));
#32236=CARTESIAN_POINT('',(-0.0258923846327359,0.0303108891324553,0.0857467461017925));
#32237=CARTESIAN_POINT('',(-0.0258923846327359,0.0280621564475424,0.0858790377684592));
#32238=CARTESIAN_POINT('',(-0.0247680182902794,0.0261146968160874,0.0860113294351258));
#32239=CARTESIAN_POINT('',(-0.023643651947823,0.0241672371846324,0.0861436211017925));
#32240=CARTESIAN_POINT('',(-0.021696192316368,0.023042870842176,0.0862759127684591));
#32241=CARTESIAN_POINT('',(-0.019748732684913,0.0219185044997195,0.0864082044351258));
#32242=CARTESIAN_POINT('',(-0.0175,0.0219185044997195,0.0865404961017925));
#32243=CARTESIAN_POINT('',(-0.0152512673150871,0.0219185044997195,0.0866727877684591));
#32244=CARTESIAN_POINT('',(-0.0133038076836321,0.023042870842176,0.0868050794351258));
#32245=CARTESIAN_POINT('',(-0.0113563480521771,0.0241672371846324,0.0869373711017925));
#32246=CARTESIAN_POINT('',(-0.0102319817097207,0.0261146968160874,0.0870696627684591));
#32247=CARTESIAN_POINT('',(-0.00910761536726419,0.0280621564475424,0.0872019544351259));
#32248=CARTESIAN_POINT('',(-0.00910761536726419,0.0303108891324553,0.0873342461017925));
#32249=CARTESIAN_POINT('',(-0.00910761536726419,0.0325596218173683,0.0874665377684592));
#32250=CARTESIAN_POINT('',(-0.0102319817097207,0.0345070814488233,0.0875988294351258));
#32251=CARTESIAN_POINT('',(-0.0113563480521771,0.0364545410802783,0.0877311211017925));
#32252=CARTESIAN_POINT('',(-0.0133038076836321,0.0375789074227347,0.0878634127684591));
#32253=CARTESIAN_POINT('',(-0.0152512673150871,0.0387032737651912,0.0879957044351258));
#32254=CARTESIAN_POINT('',(-0.0175,0.0387032737651912,0.0881279961017925));
#32255=CARTESIAN_POINT('',(-0.019748732684913,0.0387032737651912,0.0882602877684591));
#32256=CARTESIAN_POINT('',(-0.0216961923163679,0.0375789074227348,0.0883925794351258));
#32257=CARTESIAN_POINT('',(-0.023643651947823,0.0364545410802783,0.0885248711017924));
#32258=CARTESIAN_POINT('',(-0.0247680182902794,0.0345070814488233,0.0886571627684591));
#32259=CARTESIAN_POINT('',(-0.0258923846327359,0.0325596218173683,0.0887894544351259));
#32260=CARTESIAN_POINT('',(-0.0258923846327359,0.0303108891324553,0.0889217461017925));
#32261=CARTESIAN_POINT('',(-0.0258923846327359,0.0280621564475424,0.0890540377684592));
#32262=CARTESIAN_POINT('',(-0.0247680182902794,0.0261146968160874,0.0891863294351258));
#32263=CARTESIAN_POINT('',(-0.023643651947823,0.0241672371846324,0.0893186211017925));
#32264=CARTESIAN_POINT('',(-0.021696192316368,0.023042870842176,0.0894509127684591));
#32265=CARTESIAN_POINT('',(-0.019748732684913,0.0219185044997195,0.0895832044351258));
#32266=CARTESIAN_POINT('',(-0.0175,0.0219185044997195,0.0897154961017925));
#32267=CARTESIAN_POINT('',(-0.0152512673150871,0.0219185044997195,0.0898477877684591));
#32268=CARTESIAN_POINT('',(-0.0133038076836321,0.023042870842176,0.0899800794351258));
#32269=CARTESIAN_POINT('',(-0.0113563480521771,0.0241672371846324,0.0901123711017924));
#32270=CARTESIAN_POINT('',(-0.0102319817097207,0.0261146968160874,0.0902446627684591));
#32271=CARTESIAN_POINT('',(-0.00910761536726419,0.0280621564475424,0.0903769544351259));
#32272=CARTESIAN_POINT('',(-0.00910761536726419,0.0303108891324553,0.0905092461017925));
#32273=CARTESIAN_POINT('',(-0.00910761536726419,0.0325596218173683,0.0906415377684592));
#32274=CARTESIAN_POINT('',(-0.0102319817097207,0.0345070814488233,0.0907738294351258));
#32275=CARTESIAN_POINT('',(-0.0113563480521771,0.0364545410802783,0.0909061211017925));
#32276=CARTESIAN_POINT('',(-0.0133038076836321,0.0375789074227347,0.0910384127684591));
#32277=CARTESIAN_POINT('',(-0.0152512673150871,0.0387032737651912,0.0911707044351258));
#32278=CARTESIAN_POINT('',(-0.0175,0.0387032737651912,0.0913029961017925));
#32279=CARTESIAN_POINT('',(-0.019748732684913,0.0387032737651912,0.0914352877684591));
#32280=CARTESIAN_POINT('',(-0.0216961923163679,0.0375789074227348,0.0915675794351258));
#32281=CARTESIAN_POINT('',(-0.0226539774004862,0.0370259299465933,0.0916326421368322));
#32282=CARTESIAN_POINT('',(-0.0234358084101918,0.0362437045131391,0.0917));
#32283=CARTESIAN_POINT('',(-0.00910761536726419,0.0303108891324553,0.0841592461017925));
#32284=CARTESIAN_POINT('',(-0.0234358084101918,0.0362437045131391,0.0917));
#32285=CARTESIAN_POINT('',(-0.0234358084101918,0.0362437045131391,0.0917));
#32286=CARTESIAN_POINT('',(-0.0251331818648351,0.0347404540104153,0.0917));
#32287=CARTESIAN_POINT('',(-0.0261619940731697,0.0325741608248562,0.0917));
#32288=CARTESIAN_POINT('',(-0.0262891307345282,0.0303108891324569,0.0917));
#32289=CARTESIAN_POINT('',(-0.0262891307345283,0.0303108891324572,0.0917));
#32290=CARTESIAN_POINT('',(-0.0264009730508963,0.0303108891324564,0.0915881576836321));
#32291=CARTESIAN_POINT('',(-0.0087974,0.0303108891324553,0.0838490307345283));
#32292=CARTESIAN_POINT('',(-0.00910761536726419,0.0303108891324553,0.0841592461017925));
#32293=CARTESIAN_POINT('',(-0.00910761536726419,0.0325596218173683,0.0842915377684592));
#32294=CARTESIAN_POINT('',(-0.0102319817097207,0.0345070814488233,0.0844238294351258));
#32295=CARTESIAN_POINT('',(-0.0113563480521771,0.0364545410802783,0.0845561211017925));
#32296=CARTESIAN_POINT('',(-0.0133038076836321,0.0375789074227347,0.0846884127684591));
#32297=CARTESIAN_POINT('',(-0.0152512673150871,0.0387032737651912,0.0848207044351258));
#32298=CARTESIAN_POINT('',(-0.0175,0.0387032737651912,0.0849529961017925));
#32299=CARTESIAN_POINT('',(-0.019748732684913,0.0387032737651912,0.0850852877684591));
#32300=CARTESIAN_POINT('',(-0.0216961923163679,0.0375789074227348,0.0852175794351258));
#32301=CARTESIAN_POINT('',(-0.023643651947823,0.0364545410802783,0.0853498711017925));
#32302=CARTESIAN_POINT('',(-0.0247680182902794,0.0345070814488233,0.0854821627684591));
#32303=CARTESIAN_POINT('',(-0.0258923846327359,0.0325596218173683,0.0856144544351258));
#32304=CARTESIAN_POINT('',(-0.0258923846327359,0.0303108891324553,0.0857467461017925));
#32305=CARTESIAN_POINT('',(-0.0258923846327359,0.0280621564475424,0.0858790377684592));
#32306=CARTESIAN_POINT('',(-0.0247680182902794,0.0261146968160874,0.0860113294351258));
#32307=CARTESIAN_POINT('',(-0.023643651947823,0.0241672371846324,0.0861436211017925));
#32308=CARTESIAN_POINT('',(-0.021696192316368,0.023042870842176,0.0862759127684591));
#32309=CARTESIAN_POINT('',(-0.019748732684913,0.0219185044997195,0.0864082044351258));
#32310=CARTESIAN_POINT('',(-0.0175,0.0219185044997195,0.0865404961017925));
#32311=CARTESIAN_POINT('',(-0.0152512673150871,0.0219185044997195,0.0866727877684591));
#32312=CARTESIAN_POINT('',(-0.0133038076836321,0.023042870842176,0.0868050794351258));
#32313=CARTESIAN_POINT('',(-0.0113563480521771,0.0241672371846324,0.0869373711017925));
#32314=CARTESIAN_POINT('',(-0.0102319817097207,0.0261146968160874,0.0870696627684591));
#32315=CARTESIAN_POINT('',(-0.00910761536726419,0.0280621564475424,0.0872019544351259));
#32316=CARTESIAN_POINT('',(-0.00910761536726419,0.0303108891324553,0.0873342461017925));
#32317=CARTESIAN_POINT('',(-0.00910761536726419,0.0325596218173683,0.0874665377684592));
#32318=CARTESIAN_POINT('',(-0.0102319817097207,0.0345070814488233,0.0875988294351258));
#32319=CARTESIAN_POINT('',(-0.0113563480521771,0.0364545410802783,0.0877311211017925));
#32320=CARTESIAN_POINT('',(-0.0133038076836321,0.0375789074227347,0.0878634127684591));
#32321=CARTESIAN_POINT('',(-0.0152512673150871,0.0387032737651912,0.0879957044351258));
#32322=CARTESIAN_POINT('',(-0.0175,0.0387032737651912,0.0881279961017925));
#32323=CARTESIAN_POINT('',(-0.019748732684913,0.0387032737651912,0.0882602877684591));
#32324=CARTESIAN_POINT('',(-0.0216961923163679,0.0375789074227348,0.0883925794351258));
#32325=CARTESIAN_POINT('',(-0.023643651947823,0.0364545410802783,0.0885248711017924));
#32326=CARTESIAN_POINT('',(-0.0247680182902794,0.0345070814488233,0.0886571627684591));
#32327=CARTESIAN_POINT('',(-0.0258923846327359,0.0325596218173683,0.0887894544351258));
#32328=CARTESIAN_POINT('',(-0.0258923846327359,0.0303108891324553,0.0889217461017925));
#32329=CARTESIAN_POINT('',(-0.0258923846327359,0.0280621564475424,0.0890540377684592));
#32330=CARTESIAN_POINT('',(-0.0247680182902794,0.0261146968160874,0.0891863294351258));
#32331=CARTESIAN_POINT('',(-0.023643651947823,0.0241672371846324,0.0893186211017925));
#32332=CARTESIAN_POINT('',(-0.021696192316368,0.023042870842176,0.0894509127684591));
#32333=CARTESIAN_POINT('',(-0.019748732684913,0.0219185044997195,0.0895832044351258));
#32334=CARTESIAN_POINT('',(-0.0175,0.0219185044997195,0.0897154961017925));
#32335=CARTESIAN_POINT('',(-0.0152512673150871,0.0219185044997195,0.0898477877684591));
#32336=CARTESIAN_POINT('',(-0.0133038076836321,0.023042870842176,0.0899800794351258));
#32337=CARTESIAN_POINT('',(-0.0113563480521771,0.0241672371846324,0.0901123711017924));
#32338=CARTESIAN_POINT('',(-0.0102319817097207,0.0261146968160874,0.0902446627684591));
#32339=CARTESIAN_POINT('',(-0.00910761536726419,0.0280621564475424,0.0903769544351259));
#32340=CARTESIAN_POINT('',(-0.00910761536726419,0.0303108891324553,0.0905092461017925));
#32341=CARTESIAN_POINT('',(-0.00910761536726419,0.0325596218173683,0.0906415377684592));
#32342=CARTESIAN_POINT('',(-0.0102319817097207,0.0345070814488233,0.0907738294351258));
#32343=CARTESIAN_POINT('',(-0.0113563480521771,0.0364545410802783,0.0909061211017925));
#32344=CARTESIAN_POINT('',(-0.0133038076836321,0.0375789074227347,0.0910384127684591));
#32345=CARTESIAN_POINT('',(-0.0152512673150871,0.0387032737651912,0.0911707044351258));
#32346=CARTESIAN_POINT('',(-0.0175,0.0387032737651912,0.0913029961017925));
#32347=CARTESIAN_POINT('',(-0.019748732684913,0.0387032737651912,0.0914352877684591));
#32348=CARTESIAN_POINT('',(-0.0216961923163679,0.0375789074227348,0.0915675794351258));
#32349=CARTESIAN_POINT('',(-0.0229888949513052,0.0368325652084716,0.0916553932122732));
#32350=CARTESIAN_POINT('',(-0.0239449665364756,0.0356862520195069,0.091745934795067));
#32351=CARTESIAN_POINT('',(-0.00925242797917949,0.0303108891324554,0.0843040587137078));
#32352=CARTESIAN_POINT('',(-0.00925242797917948,0.0325208193949517,0.0844363503803744));
#32353=CARTESIAN_POINT('',(-0.0103573931104277,0.0344346751428656,0.0845686420470411));
#32354=CARTESIAN_POINT('',(-0.0114623582416759,0.0363485308907795,0.0847009337137078));
#32355=CARTESIAN_POINT('',(-0.0133762139895898,0.0374534960220277,0.0848332253803744));
#32356=CARTESIAN_POINT('',(-0.0152900697375036,0.0385584611532759,0.0849655170470411));
#32357=CARTESIAN_POINT('',(-0.0175000000000001,0.0385584611532759,0.0850978087137078));
#32358=CARTESIAN_POINT('',(-0.0197099302624964,0.0385584611532759,0.0852301003803745));
#32359=CARTESIAN_POINT('',(-0.0216237860104103,0.0374534960220277,0.0853623920470411));
#32360=CARTESIAN_POINT('',(-0.0235376417583242,0.0363485308907795,0.0854946837137077));
#32361=CARTESIAN_POINT('',(-0.0246426068895724,0.0344346751428656,0.0856269753803744));
#32362=CARTESIAN_POINT('',(-0.0257475720208206,0.0325208193949517,0.0857592670470411));
#32363=CARTESIAN_POINT('',(-0.0257475720208206,0.0303108891324554,0.0858915587137078));
#32364=CARTESIAN_POINT('',(-0.0257475720208206,0.028100958869959,0.0860238503803745));
#32365=CARTESIAN_POINT('',(-0.0246426068895724,0.0261871031220451,0.0861561420470411));
#32366=CARTESIAN_POINT('',(-0.0235376417583242,0.0242732473741312,0.0862884337137078));
#32367=CARTESIAN_POINT('',(-0.0216237860104103,0.023168282242883,0.0864207253803744));
#32368=CARTESIAN_POINT('',(-0.0197099302624964,0.0220633171116348,0.0865530170470411));
#32369=CARTESIAN_POINT('',(-0.0175000000000001,0.0220633171116348,0.0866853087137078));
#32370=CARTESIAN_POINT('',(-0.0152900697375037,0.0220633171116348,0.0868176003803744));
#32371=CARTESIAN_POINT('',(-0.0133762139895898,0.023168282242883,0.0869498920470411));
#32372=CARTESIAN_POINT('',(-0.0114623582416759,0.0242732473741312,0.0870821837137078));
#32373=CARTESIAN_POINT('',(-0.0103573931104277,0.026187103122045,0.0872144753803745));
#32374=CARTESIAN_POINT('',(-0.0092524279791795,0.0281009588699589,0.0873467670470411));
#32375=CARTESIAN_POINT('',(-0.00925242797917949,0.0303108891324554,0.0874790587137078));
#32376=CARTESIAN_POINT('',(-0.00925242797917948,0.0325208193949517,0.0876113503803744));
#32377=CARTESIAN_POINT('',(-0.0103573931104277,0.0344346751428656,0.0877436420470411));
#32378=CARTESIAN_POINT('',(-0.0114623582416759,0.0363485308907795,0.0878759337137077));
#32379=CARTESIAN_POINT('',(-0.0133762139895898,0.0374534960220277,0.0880082253803745));
#32380=CARTESIAN_POINT('',(-0.0152900697375036,0.0385584611532759,0.088140517047041));
#32381=CARTESIAN_POINT('',(-0.0175000000000001,0.0385584611532759,0.0882728087137078));
#32382=CARTESIAN_POINT('',(-0.0197099302624964,0.0385584611532759,0.0884051003803744));
#32383=CARTESIAN_POINT('',(-0.0216237860104103,0.0374534960220277,0.0885373920470411));
#32384=CARTESIAN_POINT('',(-0.0235376417583242,0.0363485308907795,0.0886696837137077));
#32385=CARTESIAN_POINT('',(-0.0246426068895724,0.0344346751428656,0.0888019753803745));
#32386=CARTESIAN_POINT('',(-0.0257475720208206,0.0325208193949517,0.088934267047041));
#32387=CARTESIAN_POINT('',(-0.0257475720208206,0.0303108891324554,0.0890665587137078));
#32388=CARTESIAN_POINT('',(-0.0257475720208206,0.028100958869959,0.0891988503803744));
#32389=CARTESIAN_POINT('',(-0.0246426068895724,0.0261871031220451,0.0893311420470412));
#32390=CARTESIAN_POINT('',(-0.0235376417583242,0.0242732473741312,0.0894634337137077));
#32391=CARTESIAN_POINT('',(-0.0216237860104103,0.023168282242883,0.0895957253803744));
#32392=CARTESIAN_POINT('',(-0.0197099302624964,0.0220633171116348,0.0897280170470411));
#32393=CARTESIAN_POINT('',(-0.0175000000000001,0.0220633171116348,0.0898603087137078));
#32394=CARTESIAN_POINT('',(-0.0152900697375037,0.0220633171116348,0.0899926003803744));
#32395=CARTESIAN_POINT('',(-0.0133762139895898,0.023168282242883,0.0901248920470411));
#32396=CARTESIAN_POINT('',(-0.0114623582416759,0.0242732473741312,0.0902571837137077));
#32397=CARTESIAN_POINT('',(-0.0103573931104277,0.026187103122045,0.0903894753803744));
#32398=CARTESIAN_POINT('',(-0.0092524279791795,0.0281009588699589,0.0905217670470411));
#32399=CARTESIAN_POINT('',(-0.00925242797917949,0.0303108891324554,0.0906540587137077));
#32400=CARTESIAN_POINT('',(-0.00925242797917948,0.0325208193949517,0.0907863503803744));
#32401=CARTESIAN_POINT('',(-0.0103573931104277,0.0344346751428656,0.0909186420470411));
#32402=CARTESIAN_POINT('',(-0.0114623582416759,0.0363485308907795,0.0910509337137077));
#32403=CARTESIAN_POINT('',(-0.0133762139895898,0.0374534960220277,0.0911832253803744));
#32404=CARTESIAN_POINT('',(-0.0152900697375036,0.0385584611532759,0.0913155170470411));
#32405=CARTESIAN_POINT('',(-0.0175000000000001,0.0385584611532759,0.0914478087137078));
#32406=CARTESIAN_POINT('',(-0.0197099302624964,0.0385584611532759,0.0915801003803744));
#32407=CARTESIAN_POINT('',(-0.0216237860104103,0.0374534960220277,0.0917123920470411));
#32408=CARTESIAN_POINT('',(-0.0228941827509936,0.0367200321218743,0.0918002058241885));
#32409=CARTESIAN_POINT('',(-0.0238337570914016,0.035593498842224,0.0918907474069823));
#32410=CARTESIAN_POINT('',(-0.00933080000000004,0.0303108891324554,0.0844932655092833));
#32411=CARTESIAN_POINT('',(-0.00933080000000003,0.0324998196752636,0.08462555717595));
#32412=CARTESIAN_POINT('',(-0.0104252652714042,0.0343954891324553,0.0847578488426167));
#32413=CARTESIAN_POINT('',(-0.0115197305428084,0.036291158589647,0.0848901405092833));
#32414=CARTESIAN_POINT('',(-0.0134154,0.0373856238610512,0.08502243217595));
#32415=CARTESIAN_POINT('',(-0.0153110694571917,0.0384800891324553,0.0851547238426166));
#32416=CARTESIAN_POINT('',(-0.0175000000000001,0.0384800891324554,0.0852870155092833));
#32417=CARTESIAN_POINT('',(-0.0196889305428084,0.0384800891324553,0.08541930717595));
#32418=CARTESIAN_POINT('',(-0.0215846000000001,0.0373856238610512,0.0855515988426167));
#32419=CARTESIAN_POINT('',(-0.0234802694571917,0.036291158589647,0.0856838905092833));
#32420=CARTESIAN_POINT('',(-0.0245747347285959,0.0343954891324554,0.08581618217595));
#32421=CARTESIAN_POINT('',(-0.0256692,0.0324998196752637,0.0859484738426166));
#32422=CARTESIAN_POINT('',(-0.0256692000000001,0.0303108891324554,0.0860807655092833));
#32423=CARTESIAN_POINT('',(-0.0256692000000001,0.028121958589647,0.08621305717595));
#32424=CARTESIAN_POINT('',(-0.0245747347285959,0.0262262891324554,0.0863453488426167));
#32425=CARTESIAN_POINT('',(-0.0234802694571917,0.0243306196752637,0.0864776405092833));
#32426=CARTESIAN_POINT('',(-0.0215846000000001,0.0232361544038595,0.08660993217595));
#32427=CARTESIAN_POINT('',(-0.0196889305428084,0.0221416891324553,0.0867422238426167));
#32428=CARTESIAN_POINT('',(-0.0175000000000001,0.0221416891324553,0.0868745155092834));
#32429=CARTESIAN_POINT('',(-0.0153110694571917,0.0221416891324553,0.08700680717595));
#32430=CARTESIAN_POINT('',(-0.0134154000000001,0.0232361544038595,0.0871390988426167));
#32431=CARTESIAN_POINT('',(-0.0115197305428084,0.0243306196752637,0.0872713905092833));
#32432=CARTESIAN_POINT('',(-0.0104252652714042,0.0262262891324553,0.08740368217595));
#32433=CARTESIAN_POINT('',(-0.00933080000000004,0.028121958589647,0.0875359738426167));
#32434=CARTESIAN_POINT('',(-0.00933080000000004,0.0303108891324554,0.0876682655092834));
#32435=CARTESIAN_POINT('',(-0.00933080000000003,0.0324998196752636,0.08780055717595));
#32436=CARTESIAN_POINT('',(-0.0104252652714042,0.0343954891324553,0.0879328488426166));
#32437=CARTESIAN_POINT('',(-0.0115197305428084,0.036291158589647,0.0880651405092833));
#32438=CARTESIAN_POINT('',(-0.0134154,0.0373856238610512,0.0881974321759499));
#32439=CARTESIAN_POINT('',(-0.0153110694571917,0.0384800891324553,0.0883297238426167));
#32440=CARTESIAN_POINT('',(-0.0175000000000001,0.0384800891324554,0.0884620155092833));
#32441=CARTESIAN_POINT('',(-0.0196889305428084,0.0384800891324553,0.08859430717595));
#32442=CARTESIAN_POINT('',(-0.0215846000000001,0.0373856238610512,0.0887265988426167));
#32443=CARTESIAN_POINT('',(-0.0234802694571917,0.036291158589647,0.0888588905092832));
#32444=CARTESIAN_POINT('',(-0.0245747347285959,0.0343954891324554,0.08899118217595));
#32445=CARTESIAN_POINT('',(-0.0256692,0.0324998196752637,0.0891234738426166));
#32446=CARTESIAN_POINT('',(-0.0256692000000001,0.0303108891324554,0.0892557655092833));
#32447=CARTESIAN_POINT('',(-0.0256692000000001,0.028121958589647,0.0893880571759499));
#32448=CARTESIAN_POINT('',(-0.0245747347285959,0.0262262891324554,0.0895203488426166));
#32449=CARTESIAN_POINT('',(-0.0234802694571917,0.0243306196752637,0.0896526405092834));
#32450=CARTESIAN_POINT('',(-0.0215846000000001,0.0232361544038595,0.08978493217595));
#32451=CARTESIAN_POINT('',(-0.0196889305428084,0.0221416891324553,0.0899172238426166));
#32452=CARTESIAN_POINT('',(-0.0175000000000001,0.0221416891324553,0.0900495155092833));
#32453=CARTESIAN_POINT('',(-0.0153110694571917,0.0221416891324553,0.0901818071759499));
#32454=CARTESIAN_POINT('',(-0.0134154000000001,0.0232361544038595,0.0903140988426166));
#32455=CARTESIAN_POINT('',(-0.0115197305428084,0.0243306196752637,0.0904463905092833));
#32456=CARTESIAN_POINT('',(-0.0104252652714042,0.0262262891324553,0.09057868217595));
#32457=CARTESIAN_POINT('',(-0.00933080000000004,0.028121958589647,0.0907109738426166));
#32458=CARTESIAN_POINT('',(-0.00933080000000004,0.0303108891324554,0.0908432655092833));
#32459=CARTESIAN_POINT('',(-0.00933080000000003,0.0324998196752636,0.0909755571759499));
#32460=CARTESIAN_POINT('',(-0.0104252652714042,0.0343954891324553,0.0911078488426166));
#32461=CARTESIAN_POINT('',(-0.0115197305428084,0.036291158589647,0.0912401405092833));
#32462=CARTESIAN_POINT('',(-0.0134154,0.0373856238610512,0.09137243217595));
#32463=CARTESIAN_POINT('',(-0.0153110694571917,0.0384800891324553,0.0915047238426166));
#32464=CARTESIAN_POINT('',(-0.0175000000000001,0.0384800891324554,0.0916370155092833));
#32465=CARTESIAN_POINT('',(-0.0196889305428084,0.0384800891324553,0.0917693071759499));
#32466=CARTESIAN_POINT('',(-0.0215846000000001,0.0373856238610512,0.0919015988426167));
#32467=CARTESIAN_POINT('',(-0.0228429248775488,0.0366591296542704,0.0919894126197641));
#32468=CARTESIAN_POINT('',(-0.0237735709734282,0.0355433011844023,0.0920799542025578));
#32469=CARTESIAN_POINT('',(-0.0093308,0.0303108891324553,0.0846980614690566));
#32470=CARTESIAN_POINT('',(-0.00933080000000004,0.0324998196752637,0.0848303531357232));
#32471=CARTESIAN_POINT('',(-0.0104252652714042,0.0343954891324554,0.0849626448023899));
#32472=CARTESIAN_POINT('',(-0.0115197305428084,0.036291158589647,0.0850949364690567));
#32473=CARTESIAN_POINT('',(-0.0134154,0.0373856238610511,0.0852272281357233));
#32474=CARTESIAN_POINT('',(-0.0153110694571917,0.0384800891324553,0.08535951980239));
#32475=CARTESIAN_POINT('',(-0.0175,0.0384800891324554,0.0854918114690566));
#32476=CARTESIAN_POINT('',(-0.0196889305428084,0.0384800891324554,0.0856241031357233));
#32477=CARTESIAN_POINT('',(-0.0215846,0.0373856238610512,0.0857563948023899));
#32478=CARTESIAN_POINT('',(-0.0234802694571917,0.036291158589647,0.0858886864690566));
#32479=CARTESIAN_POINT('',(-0.0245747347285959,0.0343954891324554,0.0860209781357233));
#32480=CARTESIAN_POINT('',(-0.0256692000000001,0.0324998196752637,0.0861532698023899));
#32481=CARTESIAN_POINT('',(-0.0256692,0.0303108891324553,0.0862855614690566));
#32482=CARTESIAN_POINT('',(-0.0256692000000001,0.028121958589647,0.0864178531357234));
#32483=CARTESIAN_POINT('',(-0.0245747347285959,0.0262262891324554,0.0865501448023899));
#32484=CARTESIAN_POINT('',(-0.0234802694571917,0.0243306196752637,0.0866824364690567));
#32485=CARTESIAN_POINT('',(-0.0215846,0.0232361544038595,0.0868147281357233));
#32486=CARTESIAN_POINT('',(-0.0196889305428084,0.0221416891324553,0.08694701980239));
#32487=CARTESIAN_POINT('',(-0.0175,0.0221416891324554,0.0870793114690566));
#32488=CARTESIAN_POINT('',(-0.0153110694571917,0.0221416891324553,0.0872116031357233));
#32489=CARTESIAN_POINT('',(-0.0134154,0.0232361544038595,0.0873438948023899));
#32490=CARTESIAN_POINT('',(-0.0115197305428084,0.0243306196752637,0.0874761864690566));
#32491=CARTESIAN_POINT('',(-0.0104252652714042,0.0262262891324553,0.0876084781357233));
#32492=CARTESIAN_POINT('',(-0.00933080000000005,0.028121958589647,0.0877407698023899));
#32493=CARTESIAN_POINT('',(-0.0093308,0.0303108891324553,0.0878730614690566));
#32494=CARTESIAN_POINT('',(-0.00933080000000004,0.0324998196752637,0.0880053531357233));
#32495=CARTESIAN_POINT('',(-0.0104252652714042,0.0343954891324554,0.0881376448023899));
#32496=CARTESIAN_POINT('',(-0.0115197305428084,0.036291158589647,0.0882699364690567));
#32497=CARTESIAN_POINT('',(-0.0134154,0.0373856238610511,0.0884022281357233));
#32498=CARTESIAN_POINT('',(-0.0153110694571917,0.0384800891324553,0.08853451980239));
#32499=CARTESIAN_POINT('',(-0.0175,0.0384800891324554,0.0886668114690566));
#32500=CARTESIAN_POINT('',(-0.0196889305428084,0.0384800891324554,0.0887991031357233));
#32501=CARTESIAN_POINT('',(-0.0215846,0.0373856238610512,0.0889313948023899));
#32502=CARTESIAN_POINT('',(-0.0234802694571917,0.036291158589647,0.0890636864690566));
#32503=CARTESIAN_POINT('',(-0.0245747347285959,0.0343954891324554,0.0891959781357233));
#32504=CARTESIAN_POINT('',(-0.0256692000000001,0.0324998196752637,0.0893282698023899));
#32505=CARTESIAN_POINT('',(-0.0256692,0.0303108891324553,0.0894605614690566));
#32506=CARTESIAN_POINT('',(-0.0256692000000001,0.028121958589647,0.0895928531357233));
#32507=CARTESIAN_POINT('',(-0.0245747347285959,0.0262262891324554,0.0897251448023899));
#32508=CARTESIAN_POINT('',(-0.0234802694571917,0.0243306196752637,0.0898574364690567));
#32509=CARTESIAN_POINT('',(-0.0215846,0.0232361544038595,0.0899897281357233));
#32510=CARTESIAN_POINT('',(-0.0196889305428084,0.0221416891324553,0.09012201980239));
#32511=CARTESIAN_POINT('',(-0.0175,0.0221416891324554,0.0902543114690566));
#32512=CARTESIAN_POINT('',(-0.0153110694571917,0.0221416891324553,0.0903866031357233));
#32513=CARTESIAN_POINT('',(-0.0134154,0.0232361544038595,0.0905188948023899));
#32514=CARTESIAN_POINT('',(-0.0115197305428084,0.0243306196752637,0.0906511864690566));
#32515=CARTESIAN_POINT('',(-0.0104252652714042,0.0262262891324553,0.0907834781357233));
#32516=CARTESIAN_POINT('',(-0.00933080000000005,0.028121958589647,0.0909157698023899));
#32517=CARTESIAN_POINT('',(-0.0093308,0.0303108891324553,0.0910480614690566));
#32518=CARTESIAN_POINT('',(-0.00933080000000004,0.0324998196752637,0.0911803531357234));
#32519=CARTESIAN_POINT('',(-0.0104252652714042,0.0343954891324554,0.0913126448023899));
#32520=CARTESIAN_POINT('',(-0.0115197305428084,0.036291158589647,0.0914449364690567));
#32521=CARTESIAN_POINT('',(-0.0134154,0.0373856238610511,0.0915772281357233));
#32522=CARTESIAN_POINT('',(-0.0153110694571917,0.0384800891324553,0.09170951980239));
#32523=CARTESIAN_POINT('',(-0.0175,0.0384800891324554,0.0918418114690566));
#32524=CARTESIAN_POINT('',(-0.0196889305428084,0.0384800891324554,0.0919741031357233));
#32525=CARTESIAN_POINT('',(-0.0215846,0.0373856238610512,0.0921063948023899));
#32526=CARTESIAN_POINT('',(-0.0228429248775487,0.0366591296542704,0.0921942085795374));
#32527=CARTESIAN_POINT('',(-0.0237735709734282,0.0355433011844023,0.0922847501623312));
#32528=CARTESIAN_POINT('',(-0.0093308,0.0303108891324553,0.0846980614690566));
#32529=CARTESIAN_POINT('',(-0.00933080000000005,0.0324998196752637,0.0848303531357232));
#32530=CARTESIAN_POINT('',(-0.0104252652714042,0.0343954891324554,0.0849626448023899));
#32531=CARTESIAN_POINT('',(-0.0115197305428084,0.036291158589647,0.0850949364690567));
#32532=CARTESIAN_POINT('',(-0.0134154,0.0373856238610511,0.0852272281357233));
#32533=CARTESIAN_POINT('',(-0.0153110694571917,0.0384800891324553,0.08535951980239));
#32534=CARTESIAN_POINT('',(-0.0175,0.0384800891324554,0.0854918114690566));
#32535=CARTESIAN_POINT('',(-0.0196889305428084,0.0384800891324554,0.0856241031357233));
#32536=CARTESIAN_POINT('',(-0.0215846,0.0373856238610512,0.0857563948023899));
#32537=CARTESIAN_POINT('',(-0.0234802694571917,0.036291158589647,0.0858886864690566));
#32538=CARTESIAN_POINT('',(-0.0245747347285959,0.0343954891324554,0.0860209781357233));
#32539=CARTESIAN_POINT('',(-0.0256692000000001,0.0324998196752637,0.0861532698023899));
#32540=CARTESIAN_POINT('',(-0.0256692,0.0303108891324553,0.0862855614690566));
#32541=CARTESIAN_POINT('',(-0.0256692000000001,0.028121958589647,0.0864178531357234));
#32542=CARTESIAN_POINT('',(-0.0245747347285959,0.0262262891324554,0.0865501448023899));
#32543=CARTESIAN_POINT('',(-0.0234802694571917,0.0243306196752637,0.0866824364690567));
#32544=CARTESIAN_POINT('',(-0.0215846,0.0232361544038595,0.0868147281357233));
#32545=CARTESIAN_POINT('',(-0.0196889305428084,0.0221416891324553,0.08694701980239));
#32546=CARTESIAN_POINT('',(-0.0175,0.0221416891324554,0.0870793114690566));
#32547=CARTESIAN_POINT('',(-0.0153110694571917,0.0221416891324553,0.0872116031357233));
#32548=CARTESIAN_POINT('',(-0.0134154,0.0232361544038595,0.0873438948023899));
#32549=CARTESIAN_POINT('',(-0.0115197305428084,0.0243306196752637,0.0874761864690566));
#32550=CARTESIAN_POINT('',(-0.0104252652714042,0.0262262891324553,0.0876084781357233));
#32551=CARTESIAN_POINT('',(-0.00933080000000005,0.028121958589647,0.0877407698023899));
#32552=CARTESIAN_POINT('',(-0.0093308,0.0303108891324553,0.0878730614690566));
#32553=CARTESIAN_POINT('',(-0.00933080000000005,0.0324998196752637,0.0880053531357232));
#32554=CARTESIAN_POINT('',(-0.0104252652714042,0.0343954891324554,0.0881376448023899));
#32555=CARTESIAN_POINT('',(-0.0115197305428084,0.036291158589647,0.0882699364690567));
#32556=CARTESIAN_POINT('',(-0.0134154,0.0373856238610511,0.0884022281357233));
#32557=CARTESIAN_POINT('',(-0.0153110694571917,0.0384800891324553,0.08853451980239));
#32558=CARTESIAN_POINT('',(-0.0175,0.0384800891324554,0.0886668114690566));
#32559=CARTESIAN_POINT('',(-0.0196889305428084,0.0384800891324554,0.0887991031357233));
#32560=CARTESIAN_POINT('',(-0.0215846,0.0373856238610512,0.0889313948023899));
#32561=CARTESIAN_POINT('',(-0.0234802694571917,0.036291158589647,0.0890636864690566));
#32562=CARTESIAN_POINT('',(-0.0245747347285959,0.0343954891324554,0.0891959781357233));
#32563=CARTESIAN_POINT('',(-0.0256692000000001,0.0324998196752637,0.0893282698023899));
#32564=CARTESIAN_POINT('',(-0.0256692,0.0303108891324553,0.0894605614690566));
#32565=CARTESIAN_POINT('',(-0.0256692000000001,0.028121958589647,0.0895928531357233));
#32566=CARTESIAN_POINT('',(-0.0245747347285959,0.0262262891324554,0.0897251448023899));
#32567=CARTESIAN_POINT('',(-0.0234802694571917,0.0243306196752637,0.0898574364690567));
#32568=CARTESIAN_POINT('',(-0.0215846,0.0232361544038595,0.0899897281357233));
#32569=CARTESIAN_POINT('',(-0.0196889305428084,0.0221416891324553,0.09012201980239));
#32570=CARTESIAN_POINT('',(-0.0175,0.0221416891324554,0.0902543114690566));
#32571=CARTESIAN_POINT('',(-0.0153110694571917,0.0221416891324553,0.0903866031357233));
#32572=CARTESIAN_POINT('',(-0.0134154,0.0232361544038595,0.0905188948023899));
#32573=CARTESIAN_POINT('',(-0.0115197305428084,0.0243306196752637,0.0906511864690566));
#32574=CARTESIAN_POINT('',(-0.0104252652714042,0.0262262891324553,0.0907834781357233));
#32575=CARTESIAN_POINT('',(-0.00933080000000005,0.028121958589647,0.0909157698023899));
#32576=CARTESIAN_POINT('',(-0.0093308,0.0303108891324553,0.0910480614690566));
#32577=CARTESIAN_POINT('',(-0.00933080000000005,0.0324998196752637,0.0911803531357234));
#32578=CARTESIAN_POINT('',(-0.0104252652714042,0.0343954891324554,0.0913126448023899));
#32579=CARTESIAN_POINT('',(-0.0115197305428084,0.036291158589647,0.0914449364690567));
#32580=CARTESIAN_POINT('',(-0.0134154,0.0373856238610511,0.0915772281357233));
#32581=CARTESIAN_POINT('',(-0.0142798580955441,0.0378847189752167,0.0916375554263219));
#32582=CARTESIAN_POINT('',(-0.0152390568438961,0.0381609824239307,0.0917));
#32583=CARTESIAN_POINT('',(-0.0093308,0.0303108891324553,0.0846980614690566));
#32584=CARTESIAN_POINT('',(-0.0152390568438961,0.0381609824239307,0.0917));
#32585=CARTESIAN_POINT('',(-0.0152390568438961,0.0381609824239307,0.0917));
#32586=CARTESIAN_POINT('',(-0.0166557501341046,0.0385690110778415,0.0917));
#32587=CARTESIAN_POINT('',(-0.0196821427881546,0.038626058036794,0.0917000000000001));
#32588=CARTESIAN_POINT('',(-0.0223327085372635,0.0372206465255158,0.0917));
#32589=CARTESIAN_POINT('',(-0.0234358084101918,0.0362437045131391,0.0917));
#32590=CARTESIAN_POINT('',(-0.0085688,0.0303108891324553,0.0846980614690566));
#32591=CARTESIAN_POINT('',(-0.0175,0.0303108891324553,0.0863555479362832));
#32592=CARTESIAN_POINT('',(-0.0093308,0.0303108891324553,0.0850479938051895));
#32593=CARTESIAN_POINT('',(-0.00933080000000005,0.0324998196752637,0.0851802854718562));
#32594=CARTESIAN_POINT('',(-0.0104252652714042,0.0343954891324554,0.0853125771385228));
#32595=CARTESIAN_POINT('',(-0.0115197305428084,0.036291158589647,0.0854448688051895));
#32596=CARTESIAN_POINT('',(-0.0134154,0.0373856238610512,0.0855771604718562));
#32597=CARTESIAN_POINT('',(-0.0153110694571917,0.0384800891324553,0.0857094521385228));
#32598=CARTESIAN_POINT('',(-0.0175,0.0384800891324554,0.0858417438051895));
#32599=CARTESIAN_POINT('',(-0.0196889305428084,0.0384800891324554,0.0859740354718562));
#32600=CARTESIAN_POINT('',(-0.0215846,0.0373856238610512,0.0861063271385228));
#32601=CARTESIAN_POINT('',(-0.0234802694571917,0.036291158589647,0.0862386188051896));
#32602=CARTESIAN_POINT('',(-0.0245747347285959,0.0343954891324554,0.0863709104718562));
#32603=CARTESIAN_POINT('',(-0.0256692000000001,0.0324998196752637,0.0865032021385229));
#32604=CARTESIAN_POINT('',(-0.0256692,0.0303108891324553,0.0866354938051895));
#32605=CARTESIAN_POINT('',(-0.0256692000000001,0.028121958589647,0.0867677854718562));
#32606=CARTESIAN_POINT('',(-0.0245747347285959,0.0262262891324554,0.0869000771385228));
#32607=CARTESIAN_POINT('',(-0.0234802694571917,0.0243306196752637,0.0870323688051895));
#32608=CARTESIAN_POINT('',(-0.0215846,0.0232361544038595,0.0871646604718562));
#32609=CARTESIAN_POINT('',(-0.0196889305428084,0.0221416891324553,0.0872969521385228));
#32610=CARTESIAN_POINT('',(-0.0175,0.0221416891324554,0.0874292438051895));
#32611=CARTESIAN_POINT('',(-0.0153110694571917,0.0221416891324553,0.0875615354718562));
#32612=CARTESIAN_POINT('',(-0.0134154,0.0232361544038595,0.0876938271385228));
#32613=CARTESIAN_POINT('',(-0.0115197305428084,0.0243306196752637,0.0878261188051896));
#32614=CARTESIAN_POINT('',(-0.0104252652714042,0.0262262891324554,0.0879584104718562));
#32615=CARTESIAN_POINT('',(-0.00933080000000005,0.028121958589647,0.0880907021385229));
#32616=CARTESIAN_POINT('',(-0.0093308,0.0303108891324553,0.0882229938051895));
#32617=CARTESIAN_POINT('',(-0.00933080000000005,0.0324998196752637,0.0883552854718562));
#32618=CARTESIAN_POINT('',(-0.0104252652714042,0.0343954891324554,0.0884875771385228));
#32619=CARTESIAN_POINT('',(-0.0115197305428084,0.036291158589647,0.0886198688051895));
#32620=CARTESIAN_POINT('',(-0.0134154,0.0373856238610512,0.0887521604718562));
#32621=CARTESIAN_POINT('',(-0.0153110694571917,0.0384800891324553,0.0888844521385229));
#32622=CARTESIAN_POINT('',(-0.0175,0.0384800891324554,0.0890167438051895));
#32623=CARTESIAN_POINT('',(-0.0196889305428084,0.0384800891324554,0.0891490354718562));
#32624=CARTESIAN_POINT('',(-0.0215846,0.0373856238610512,0.0892813271385228));
#32625=CARTESIAN_POINT('',(-0.0234802694571917,0.036291158589647,0.0894136188051896));
#32626=CARTESIAN_POINT('',(-0.0245747347285959,0.0343954891324554,0.0895459104718562));
#32627=CARTESIAN_POINT('',(-0.0256692000000001,0.0324998196752637,0.0896782021385229));
#32628=CARTESIAN_POINT('',(-0.0256692,0.0303108891324553,0.0898104938051895));
#32629=CARTESIAN_POINT('',(-0.0256692000000001,0.028121958589647,0.0899427854718562));
#32630=CARTESIAN_POINT('',(-0.0245747347285959,0.0262262891324554,0.0900750771385228));
#32631=CARTESIAN_POINT('',(-0.0234802694571917,0.0243306196752637,0.0902073688051895));
#32632=CARTESIAN_POINT('',(-0.0215846,0.0232361544038595,0.0903396604718562));
#32633=CARTESIAN_POINT('',(-0.0196889305428084,0.0221416891324553,0.0904719521385229));
#32634=CARTESIAN_POINT('',(-0.0175,0.0221416891324554,0.0906042438051895));
#32635=CARTESIAN_POINT('',(-0.0153110694571917,0.0221416891324553,0.0907365354718562));
#32636=CARTESIAN_POINT('',(-0.0134154,0.0232361544038595,0.0908688271385228));
#32637=CARTESIAN_POINT('',(-0.0115197305428084,0.0243306196752637,0.0910011188051895));
#32638=CARTESIAN_POINT('',(-0.0104252652714042,0.0262262891324554,0.0911334104718562));
#32639=CARTESIAN_POINT('',(-0.00933080000000005,0.028121958589647,0.0912657021385229));
#32640=CARTESIAN_POINT('',(-0.0093308,0.0303108891324553,0.0913979938051895));
#32641=CARTESIAN_POINT('',(-0.00933080000000005,0.0324998196752637,0.0915302854718562));
#32642=CARTESIAN_POINT('',(-0.0104252652714042,0.0343954891324554,0.0916625771385228));
#32643=CARTESIAN_POINT('',(-0.0105787406133938,0.0346613162224903,0.0916811282148471));
#32644=CARTESIAN_POINT('',(-0.0107517314949501,0.0349148766241576,0.0917));
#32645=CARTESIAN_POINT('',(-0.0093308,0.0303108891324553,0.0850479938051895));
#32646=CARTESIAN_POINT('',(-0.0107517314949501,0.0349148766241576,0.0917));
#32647=CARTESIAN_POINT('',(-0.0175,0.0303108891324553,0.0917));
#32648=CARTESIAN_POINT('',(-0.0093308,0.0303108891324553,0.0848730276371231));
#32649=CARTESIAN_POINT('',(-0.00832342471144782,0.0303108891324553,0.085499093987987));
#32650=CARTESIAN_POINT('',(-0.008518,0.0303108891324553,0.0856623620408474));
#32651=CARTESIAN_POINT('',(-0.00847389336287265,0.0303108891324553,0.0854122208715823));
#32652=CARTESIAN_POINT('',(-0.008264,0.0303108891324553,0.0856623620408474));
#32653=CARTESIAN_POINT('',(-0.0087974,0.0303108891324553,0.0853551779230184));
#32654=CARTESIAN_POINT('',(-0.00912090663712743,0.0303108891324553,0.0852981349744546));
#32655=CARTESIAN_POINT('',(-0.0090768,0.0303108891324553,0.0850479938051895));
#32656=CARTESIAN_POINT('',(-0.008264,0.0303108891324553,0.0843311810204237));
#32657=CARTESIAN_POINT('',(-0.0175,0.0303108891324553,0.0867173896326779));
#32658=CARTESIAN_POINT('',(-0.026736,0.0303108891324553,0.09135));
#32659=CARTESIAN_POINT('',(-0.026736,0.0303108891324553,0.091));
#32660=CARTESIAN_POINT('',(-0.026736,0.0303108891324564,0.0917));
#32661=CARTESIAN_POINT('',(-0.0175,0.0303108891324553,0.0917));
#32662=CARTESIAN_POINT('',(-0.00997922046889643,0.0249497725281897,0.0917));
#32663=CARTESIAN_POINT('',(-0.0213627414806,0.0219214359766142,0.0910000000000001));
#32664=CARTESIAN_POINT('',(-0.0195241340747034,0.0210748891324554,0.0911104100162255));
#32665=CARTESIAN_POINT('',(-0.0175,0.0210748891324553,0.0912186120408473));
#32666=CARTESIAN_POINT('',(-0.0150252212587062,0.0210748891324553,0.0913509037075141));
#32667=CARTESIAN_POINT('',(-0.012882,0.0223122785031023,0.0914831953741807));
#32668=CARTESIAN_POINT('',(-0.0111440750554154,0.0233156699376896,0.0915904698735012));
#32669=CARTESIAN_POINT('',(-0.00997922046889642,0.0249497725281897,0.0916999999999999));
#32670=CARTESIAN_POINT('',(-0.0213627414806001,0.0219214359766143,0.091));
#32671=CARTESIAN_POINT('',(-0.0175,0.0303108891324553,0.091));
#32672=CARTESIAN_POINT('',(-0.0093308,0.0303108891324553,0.0850479938051895));
#32673=CARTESIAN_POINT('',(-0.00933080000000005,0.0324998196752637,0.0851802854718562));
#32674=CARTESIAN_POINT('',(-0.0104252652714042,0.0343954891324554,0.0853125771385228));
#32675=CARTESIAN_POINT('',(-0.0115197305428084,0.036291158589647,0.0854448688051895));
#32676=CARTESIAN_POINT('',(-0.0134154,0.0373856238610511,0.0855771604718562));
#32677=CARTESIAN_POINT('',(-0.0153110694571917,0.0384800891324553,0.0857094521385228));
#32678=CARTESIAN_POINT('',(-0.0175,0.0384800891324554,0.0858417438051895));
#32679=CARTESIAN_POINT('',(-0.0196889305428084,0.0384800891324553,0.0859740354718562));
#32680=CARTESIAN_POINT('',(-0.0215846,0.0373856238610512,0.0861063271385228));
#32681=CARTESIAN_POINT('',(-0.0234802694571917,0.036291158589647,0.0862386188051896));
#32682=CARTESIAN_POINT('',(-0.0245747347285959,0.0343954891324554,0.0863709104718562));
#32683=CARTESIAN_POINT('',(-0.0256692000000001,0.0324998196752637,0.0865032021385229));
#32684=CARTESIAN_POINT('',(-0.0256692,0.0303108891324553,0.0866354938051895));
#32685=CARTESIAN_POINT('',(-0.0256692000000001,0.028121958589647,0.0867677854718562));
#32686=CARTESIAN_POINT('',(-0.0245747347285959,0.0262262891324554,0.0869000771385228));
#32687=CARTESIAN_POINT('',(-0.0234802694571917,0.0243306196752637,0.0870323688051895));
#32688=CARTESIAN_POINT('',(-0.0215846,0.0232361544038595,0.0871646604718562));
#32689=CARTESIAN_POINT('',(-0.0196889305428084,0.0221416891324553,0.0872969521385228));
#32690=CARTESIAN_POINT('',(-0.0175,0.0221416891324554,0.0874292438051895));
#32691=CARTESIAN_POINT('',(-0.0153110694571917,0.0221416891324553,0.0875615354718562));
#32692=CARTESIAN_POINT('',(-0.0134154,0.0232361544038595,0.0876938271385228));
#32693=CARTESIAN_POINT('',(-0.0115197305428084,0.0243306196752637,0.0878261188051896));
#32694=CARTESIAN_POINT('',(-0.0104252652714042,0.0262262891324553,0.0879584104718562));
#32695=CARTESIAN_POINT('',(-0.00933080000000006,0.028121958589647,0.0880907021385229));
#32696=CARTESIAN_POINT('',(-0.0093308,0.0303108891324553,0.0882229938051895));
#32697=CARTESIAN_POINT('',(-0.00933080000000005,0.0324998196752637,0.0883552854718562));
#32698=CARTESIAN_POINT('',(-0.0104252652714042,0.0343954891324554,0.0884875771385228));
#32699=CARTESIAN_POINT('',(-0.0115197305428084,0.036291158589647,0.0886198688051895));
#32700=CARTESIAN_POINT('',(-0.0134154,0.0373856238610511,0.0887521604718562));
#32701=CARTESIAN_POINT('',(-0.0153110694571917,0.0384800891324553,0.0888844521385229));
#32702=CARTESIAN_POINT('',(-0.0175,0.0384800891324554,0.0890167438051895));
#32703=CARTESIAN_POINT('',(-0.0196889305428084,0.0384800891324553,0.0891490354718562));
#32704=CARTESIAN_POINT('',(-0.0215846,0.0373856238610512,0.0892813271385228));
#32705=CARTESIAN_POINT('',(-0.0234802694571917,0.036291158589647,0.0894136188051895));
#32706=CARTESIAN_POINT('',(-0.0245747347285959,0.0343954891324554,0.0895459104718562));
#32707=CARTESIAN_POINT('',(-0.0256692000000001,0.0324998196752637,0.0896782021385228));
#32708=CARTESIAN_POINT('',(-0.0256692,0.0303108891324553,0.0898104938051895));
#32709=CARTESIAN_POINT('',(-0.0256692000000001,0.028121958589647,0.0899427854718562));
#32710=CARTESIAN_POINT('',(-0.0245747347285959,0.0262262891324554,0.0900750771385228));
#32711=CARTESIAN_POINT('',(-0.0234802694571917,0.0243306196752637,0.0902073688051895));
#32712=CARTESIAN_POINT('',(-0.0215846,0.0232361544038595,0.0903396604718562));
#32713=CARTESIAN_POINT('',(-0.0196889305428084,0.0221416891324553,0.0904719521385229));
#32714=CARTESIAN_POINT('',(-0.0175,0.0221416891324554,0.0906042438051895));
#32715=CARTESIAN_POINT('',(-0.0153110694571917,0.0221416891324553,0.0907365354718562));
#32716=CARTESIAN_POINT('',(-0.0134154,0.0232361544038595,0.0908688271385228));
#32717=CARTESIAN_POINT('',(-0.0115197305428084,0.0243306196752637,0.0910011188051895));
#32718=CARTESIAN_POINT('',(-0.0104252652714042,0.0262262891324553,0.0911334104718562));
#32719=CARTESIAN_POINT('',(-0.00933080000000006,0.028121958589647,0.0912657021385229));
#32720=CARTESIAN_POINT('',(-0.0093308,0.0303108891324553,0.0913979938051895));
#32721=CARTESIAN_POINT('',(-0.00933080000000005,0.0324998196752637,0.0915302854718562));
#32722=CARTESIAN_POINT('',(-0.0104252652714042,0.0343954891324554,0.0916625771385228));
#32723=CARTESIAN_POINT('',(-0.0107406510492572,0.0349417533236814,0.0917006988690932));
#32724=CARTESIAN_POINT('',(-0.0111361563717333,0.0354331272092114,0.0917399368095904));
#32725=CARTESIAN_POINT('',(-0.00933080000000005,0.0303108891324553,0.085176952984899));
#32726=CARTESIAN_POINT('',(-0.00933080000000005,0.0324998196752637,0.0853092446515657));
#32727=CARTESIAN_POINT('',(-0.0104252652714042,0.0343954891324554,0.0854415363182324));
#32728=CARTESIAN_POINT('',(-0.0115197305428084,0.036291158589647,0.085573827984899));
#32729=CARTESIAN_POINT('',(-0.0134154,0.0373856238610512,0.0857061196515657));
#32730=CARTESIAN_POINT('',(-0.0153110694571917,0.0384800891324553,0.0858384113182323));
#32731=CARTESIAN_POINT('',(-0.0175,0.0384800891324553,0.085970702984899));
#32732=CARTESIAN_POINT('',(-0.0196889305428083,0.0384800891324553,0.0861029946515657));
#32733=CARTESIAN_POINT('',(-0.0215846,0.0373856238610512,0.0862352863182323));
#32734=CARTESIAN_POINT('',(-0.0234802694571917,0.036291158589647,0.0863675779848991));
#32735=CARTESIAN_POINT('',(-0.0245747347285959,0.0343954891324554,0.0864998696515657));
#32736=CARTESIAN_POINT('',(-0.0256692,0.0324998196752637,0.0866321613182323));
#32737=CARTESIAN_POINT('',(-0.0256692,0.0303108891324553,0.086764452984899));
#32738=CARTESIAN_POINT('',(-0.0256692000000001,0.028121958589647,0.0868967446515656));
#32739=CARTESIAN_POINT('',(-0.0245747347285959,0.0262262891324553,0.0870290363182323));
#32740=CARTESIAN_POINT('',(-0.0234802694571917,0.0243306196752637,0.087161327984899));
#32741=CARTESIAN_POINT('',(-0.0215846000000001,0.0232361544038595,0.0872936196515656));
#32742=CARTESIAN_POINT('',(-0.0196889305428084,0.0221416891324554,0.0874259113182324));
#32743=CARTESIAN_POINT('',(-0.0175,0.0221416891324554,0.087558202984899));
#32744=CARTESIAN_POINT('',(-0.0153110694571917,0.0221416891324554,0.0876904946515657));
#32745=CARTESIAN_POINT('',(-0.0134154000000001,0.0232361544038595,0.0878227863182323));
#32746=CARTESIAN_POINT('',(-0.0115197305428084,0.0243306196752637,0.0879550779848991));
#32747=CARTESIAN_POINT('',(-0.0104252652714042,0.0262262891324553,0.0880873696515656));
#32748=CARTESIAN_POINT('',(-0.00933080000000006,0.028121958589647,0.0882196613182324));
#32749=CARTESIAN_POINT('',(-0.00933080000000005,0.0303108891324553,0.088351952984899));
#32750=CARTESIAN_POINT('',(-0.00933080000000005,0.0324998196752637,0.0884842446515657));
#32751=CARTESIAN_POINT('',(-0.0104252652714042,0.0343954891324554,0.0886165363182324));
#32752=CARTESIAN_POINT('',(-0.0115197305428084,0.036291158589647,0.088748827984899));
#32753=CARTESIAN_POINT('',(-0.0134154,0.0373856238610512,0.0888811196515657));
#32754=CARTESIAN_POINT('',(-0.0153110694571917,0.0384800891324553,0.0890134113182324));
#32755=CARTESIAN_POINT('',(-0.0175,0.0384800891324553,0.089145702984899));
#32756=CARTESIAN_POINT('',(-0.0196889305428083,0.0384800891324553,0.0892779946515657));
#32757=CARTESIAN_POINT('',(-0.0215846,0.0373856238610512,0.0894102863182323));
#32758=CARTESIAN_POINT('',(-0.0234802694571917,0.036291158589647,0.089542577984899));
#32759=CARTESIAN_POINT('',(-0.0245747347285959,0.0343954891324554,0.0896748696515657));
#32760=CARTESIAN_POINT('',(-0.0256692,0.0324998196752637,0.0898071613182323));
#32761=CARTESIAN_POINT('',(-0.0256692,0.0303108891324553,0.089939452984899));
#32762=CARTESIAN_POINT('',(-0.0256692000000001,0.028121958589647,0.0900717446515657));
#32763=CARTESIAN_POINT('',(-0.0245747347285959,0.0262262891324553,0.0902040363182323));
#32764=CARTESIAN_POINT('',(-0.0234802694571917,0.0243306196752637,0.090336327984899));
#32765=CARTESIAN_POINT('',(-0.0215846000000001,0.0232361544038595,0.0904686196515656));
#32766=CARTESIAN_POINT('',(-0.0196889305428084,0.0221416891324554,0.0906009113182324));
#32767=CARTESIAN_POINT('',(-0.0175,0.0221416891324554,0.090733202984899));
#32768=CARTESIAN_POINT('',(-0.0153110694571917,0.0221416891324554,0.0908654946515656));
#32769=CARTESIAN_POINT('',(-0.0134154000000001,0.0232361544038595,0.0909977863182323));
#32770=CARTESIAN_POINT('',(-0.0115197305428084,0.0243306196752637,0.091130077984899));
#32771=CARTESIAN_POINT('',(-0.0104252652714042,0.0262262891324553,0.0912623696515656));
#32772=CARTESIAN_POINT('',(-0.00933080000000006,0.028121958589647,0.0913946613182323));
#32773=CARTESIAN_POINT('',(-0.00933080000000005,0.0303108891324553,0.0915269529848989));
#32774=CARTESIAN_POINT('',(-0.00933080000000005,0.0324998196752637,0.0916592446515657));
#32775=CARTESIAN_POINT('',(-0.0104252652714042,0.0343954891324554,0.0917915363182324));
#32776=CARTESIAN_POINT('',(-0.0107406510492572,0.0349417533236814,0.0918296580488028));
#32777=CARTESIAN_POINT('',(-0.0111361563717333,0.0354331272092114,0.0918688959893));
#32778=CARTESIAN_POINT('',(-0.00924790663712744,0.0303108891324553,0.0852757414479046));
#32779=CARTESIAN_POINT('',(-0.00924790663712744,0.0325220308849033,0.0854080331145713));
#32780=CARTESIAN_POINT('',(-0.0103534775133514,0.0344369358138916,0.085540324781238));
#32781=CARTESIAN_POINT('',(-0.0114590483895754,0.03635184074288,0.0856726164479047));
#32782=CARTESIAN_POINT('',(-0.0133739533185637,0.037457411619104,0.0858049081145713));
#32783=CARTESIAN_POINT('',(-0.0152888582475521,0.038562982495328,0.0859371997812381));
#32784=CARTESIAN_POINT('',(-0.0175,0.0385629824953279,0.0860694914479046));
#32785=CARTESIAN_POINT('',(-0.019711141752448,0.038562982495328,0.0862017831145713));
#32786=CARTESIAN_POINT('',(-0.0216260466814364,0.037457411619104,0.0863340747812379));
#32787=CARTESIAN_POINT('',(-0.0235409516104247,0.03635184074288,0.0864663664479047));
#32788=CARTESIAN_POINT('',(-0.0246465224866487,0.0344369358138917,0.0865986581145713));
#32789=CARTESIAN_POINT('',(-0.0257520933628727,0.0325220308849033,0.086730949781238));
#32790=CARTESIAN_POINT('',(-0.0257520933628726,0.0303108891324553,0.0868632414479047));
#32791=CARTESIAN_POINT('',(-0.0257520933628727,0.0280997473800074,0.0869955331145714));
#32792=CARTESIAN_POINT('',(-0.0246465224866487,0.0261848424510191,0.087127824781238));
#32793=CARTESIAN_POINT('',(-0.0235409516104247,0.0242699375220307,0.0872601164479047));
#32794=CARTESIAN_POINT('',(-0.0216260466814364,0.0231643666458067,0.0873924081145713));
#32795=CARTESIAN_POINT('',(-0.019711141752448,0.0220587957695827,0.0875246997812379));
#32796=CARTESIAN_POINT('',(-0.0175,0.0220587957695827,0.0876569914479047));
#32797=CARTESIAN_POINT('',(-0.0152888582475521,0.0220587957695827,0.0877892831145713));
#32798=CARTESIAN_POINT('',(-0.0133739533185638,0.0231643666458067,0.087921574781238));
#32799=CARTESIAN_POINT('',(-0.0114590483895754,0.0242699375220307,0.0880538664479047));
#32800=CARTESIAN_POINT('',(-0.0103534775133514,0.026184842451019,0.0881861581145713));
#32801=CARTESIAN_POINT('',(-0.00924790663712744,0.0280997473800074,0.088318449781238));
#32802=CARTESIAN_POINT('',(-0.00924790663712744,0.0303108891324553,0.0884507414479046));
#32803=CARTESIAN_POINT('',(-0.00924790663712744,0.0325220308849033,0.0885830331145714));
#32804=CARTESIAN_POINT('',(-0.0103534775133514,0.0344369358138916,0.088715324781238));
#32805=CARTESIAN_POINT('',(-0.0114590483895754,0.03635184074288,0.0888476164479046));
#32806=CARTESIAN_POINT('',(-0.0133739533185637,0.037457411619104,0.0889799081145713));
#32807=CARTESIAN_POINT('',(-0.0152888582475521,0.038562982495328,0.089112199781238));
#32808=CARTESIAN_POINT('',(-0.0175,0.0385629824953279,0.0892444914479046));
#32809=CARTESIAN_POINT('',(-0.019711141752448,0.038562982495328,0.0893767831145713));
#32810=CARTESIAN_POINT('',(-0.0216260466814364,0.037457411619104,0.0895090747812379));
#32811=CARTESIAN_POINT('',(-0.0235409516104247,0.03635184074288,0.0896413664479047));
#32812=CARTESIAN_POINT('',(-0.0246465224866487,0.0344369358138917,0.0897736581145713));
#32813=CARTESIAN_POINT('',(-0.0257520933628727,0.0325220308849033,0.0899059497812379));
#32814=CARTESIAN_POINT('',(-0.0257520933628726,0.0303108891324553,0.0900382414479046));
#32815=CARTESIAN_POINT('',(-0.0257520933628727,0.0280997473800074,0.0901705331145713));
#32816=CARTESIAN_POINT('',(-0.0246465224866487,0.0261848424510191,0.0903028247812379));
#32817=CARTESIAN_POINT('',(-0.0235409516104247,0.0242699375220307,0.0904351164479046));
#32818=CARTESIAN_POINT('',(-0.0216260466814364,0.0231643666458067,0.0905674081145714));
#32819=CARTESIAN_POINT('',(-0.019711141752448,0.0220587957695827,0.090699699781238));
#32820=CARTESIAN_POINT('',(-0.0175,0.0220587957695827,0.0908319914479047));
#32821=CARTESIAN_POINT('',(-0.0152888582475521,0.0220587957695827,0.0909642831145713));
#32822=CARTESIAN_POINT('',(-0.0133739533185638,0.0231643666458067,0.091096574781238));
#32823=CARTESIAN_POINT('',(-0.0114590483895754,0.0242699375220307,0.0912288664479047));
#32824=CARTESIAN_POINT('',(-0.0103534775133514,0.026184842451019,0.0913611581145713));
#32825=CARTESIAN_POINT('',(-0.00924790663712744,0.0280997473800074,0.091493449781238));
#32826=CARTESIAN_POINT('',(-0.00924790663712744,0.0303108891324553,0.0916257414479047));
#32827=CARTESIAN_POINT('',(-0.00924790663712744,0.0325220308849033,0.0917580331145713));
#32828=CARTESIAN_POINT('',(-0.0103534775133514,0.0344369358138916,0.091890324781238));
#32829=CARTESIAN_POINT('',(-0.0106720635296278,0.0349887429806633,0.0919284465118084));
#32830=CARTESIAN_POINT('',(-0.0110715820683569,0.0354851028665115,0.0919676844523055));
#32831=CARTESIAN_POINT('',(-0.00912090663712744,0.0303108891324553,0.0852981349744546));
#32832=CARTESIAN_POINT('',(-0.00912090663712744,0.032556060432342,0.0854304266411213));
#32833=CARTESIAN_POINT('',(-0.0102434922870708,0.0345004358138917,0.0855627183077879));
#32834=CARTESIAN_POINT('',(-0.0113660779370141,0.0364448111954412,0.0856950099744546));
#32835=CARTESIAN_POINT('',(-0.0133104533185637,0.0375673968453846,0.0858273016411213));
#32836=CARTESIAN_POINT('',(-0.0152548287001133,0.038689982495328,0.0859595933077879));
#32837=CARTESIAN_POINT('',(-0.0175,0.038689982495328,0.0860918849744546));
#32838=CARTESIAN_POINT('',(-0.0197451712998867,0.038689982495328,0.0862241766411214));
#32839=CARTESIAN_POINT('',(-0.0216895466814364,0.0375673968453846,0.0863564683077879));
#32840=CARTESIAN_POINT('',(-0.023633922062986,0.0364448111954412,0.0864887599744547));
#32841=CARTESIAN_POINT('',(-0.0247565077129293,0.0345004358138917,0.0866210516411213));
#32842=CARTESIAN_POINT('',(-0.0258790933628727,0.0325560604323421,0.086753343307788));
#32843=CARTESIAN_POINT('',(-0.0258790933628727,0.0303108891324553,0.0868856349744546));
#32844=CARTESIAN_POINT('',(-0.0258790933628727,0.0280657178325686,0.0870179266411213));
#32845=CARTESIAN_POINT('',(-0.0247565077129293,0.0261213424510191,0.087150218307788));
#32846=CARTESIAN_POINT('',(-0.023633922062986,0.0241769670694694,0.0872825099744546));
#32847=CARTESIAN_POINT('',(-0.0216895466814364,0.0230543814195261,0.0874148016411213));
#32848=CARTESIAN_POINT('',(-0.0197451712998867,0.0219317957695827,0.087547093307788));
#32849=CARTESIAN_POINT('',(-0.0175,0.0219317957695827,0.0876793849744546));
#32850=CARTESIAN_POINT('',(-0.0152548287001134,0.0219317957695827,0.0878116766411214));
#32851=CARTESIAN_POINT('',(-0.0133104533185637,0.0230543814195261,0.087943968307788));
#32852=CARTESIAN_POINT('',(-0.0113660779370141,0.0241769670694694,0.0880762599744547));
#32853=CARTESIAN_POINT('',(-0.0102434922870708,0.026121342451019,0.0882085516411213));
#32854=CARTESIAN_POINT('',(-0.00912090663712744,0.0280657178325686,0.088340843307788));
#32855=CARTESIAN_POINT('',(-0.00912090663712744,0.0303108891324553,0.0884731349744546));
#32856=CARTESIAN_POINT('',(-0.00912090663712744,0.032556060432342,0.0886054266411213));
#32857=CARTESIAN_POINT('',(-0.0102434922870708,0.0345004358138917,0.0887377183077879));
#32858=CARTESIAN_POINT('',(-0.0113660779370141,0.0364448111954412,0.0888700099744546));
#32859=CARTESIAN_POINT('',(-0.0133104533185637,0.0375673968453846,0.0890023016411213));
#32860=CARTESIAN_POINT('',(-0.0152548287001133,0.038689982495328,0.0891345933077879));
#32861=CARTESIAN_POINT('',(-0.0175,0.038689982495328,0.0892668849744546));
#32862=CARTESIAN_POINT('',(-0.0197451712998867,0.038689982495328,0.0893991766411213));
#32863=CARTESIAN_POINT('',(-0.0216895466814364,0.0375673968453846,0.089531468307788));
#32864=CARTESIAN_POINT('',(-0.023633922062986,0.0364448111954412,0.0896637599744546));
#32865=CARTESIAN_POINT('',(-0.0247565077129293,0.0345004358138917,0.0897960516411213));
#32866=CARTESIAN_POINT('',(-0.0258790933628727,0.0325560604323421,0.089928343307788));
#32867=CARTESIAN_POINT('',(-0.0258790933628727,0.0303108891324553,0.0900606349744546));
#32868=CARTESIAN_POINT('',(-0.0258790933628727,0.0280657178325686,0.0901929266411213));
#32869=CARTESIAN_POINT('',(-0.0247565077129293,0.0261213424510191,0.0903252183077879));
#32870=CARTESIAN_POINT('',(-0.023633922062986,0.0241769670694694,0.0904575099744546));
#32871=CARTESIAN_POINT('',(-0.0216895466814364,0.0230543814195261,0.0905898016411213));
#32872=CARTESIAN_POINT('',(-0.0197451712998867,0.0219317957695827,0.0907220933077879));
#32873=CARTESIAN_POINT('',(-0.0175,0.0219317957695827,0.0908543849744546));
#32874=CARTESIAN_POINT('',(-0.0152548287001134,0.0219317957695827,0.0909866766411213));
#32875=CARTESIAN_POINT('',(-0.0133104533185637,0.0230543814195261,0.0911189683077879));
#32876=CARTESIAN_POINT('',(-0.0113660779370141,0.0241769670694694,0.0912512599744547));
#32877=CARTESIAN_POINT('',(-0.0102434922870708,0.026121342451019,0.0913835516411213));
#32878=CARTESIAN_POINT('',(-0.00912090663712744,0.0280657178325686,0.091515843307788));
#32879=CARTESIAN_POINT('',(-0.00912090663712744,0.0303108891324553,0.0916481349744546));
#32880=CARTESIAN_POINT('',(-0.00912090663712744,0.032556060432342,0.0917804266411213));
#32881=CARTESIAN_POINT('',(-0.0102434922870708,0.0345004358138917,0.0919127183077879));
#32882=CARTESIAN_POINT('',(-0.010566981353069,0.0350607353118935,0.0919508400383583));
#32883=CARTESIAN_POINT('',(-0.0109726484958174,0.035564734193416,0.0919900779788555));
#32884=CARTESIAN_POINT('',(-0.00912090663712744,0.0303108891324553,0.0852981349744546));
#32885=CARTESIAN_POINT('',(-0.00912090663712744,0.032556060432342,0.0854304266411213));
#32886=CARTESIAN_POINT('',(-0.0102434922870708,0.0345004358138917,0.0855627183077879));
#32887=CARTESIAN_POINT('',(-0.0113660779370141,0.0364448111954412,0.0856950099744546));
#32888=CARTESIAN_POINT('',(-0.0133104533185637,0.0375673968453846,0.0858273016411213));
#32889=CARTESIAN_POINT('',(-0.0152548287001133,0.038689982495328,0.0859595933077879));
#32890=CARTESIAN_POINT('',(-0.0175,0.038689982495328,0.0860918849744546));
#32891=CARTESIAN_POINT('',(-0.0197451712998867,0.038689982495328,0.0862241766411212));
#32892=CARTESIAN_POINT('',(-0.0216895466814364,0.0375673968453846,0.0863564683077879));
#32893=CARTESIAN_POINT('',(-0.023633922062986,0.0364448111954412,0.0864887599744547));
#32894=CARTESIAN_POINT('',(-0.0247565077129293,0.0345004358138917,0.0866210516411213));
#32895=CARTESIAN_POINT('',(-0.0258790933628727,0.0325560604323421,0.086753343307788));
#32896=CARTESIAN_POINT('',(-0.0258790933628727,0.0303108891324553,0.0868856349744546));
#32897=CARTESIAN_POINT('',(-0.0258790933628727,0.0280657178325686,0.0870179266411213));
#32898=CARTESIAN_POINT('',(-0.0247565077129293,0.0261213424510191,0.087150218307788));
#32899=CARTESIAN_POINT('',(-0.023633922062986,0.0241769670694694,0.0872825099744546));
#32900=CARTESIAN_POINT('',(-0.0216895466814364,0.0230543814195261,0.0874148016411213));
#32901=CARTESIAN_POINT('',(-0.0197451712998867,0.0219317957695827,0.087547093307788));
#32902=CARTESIAN_POINT('',(-0.0175,0.0219317957695827,0.0876793849744546));
#32903=CARTESIAN_POINT('',(-0.0152548287001134,0.0219317957695827,0.0878116766411214));
#32904=CARTESIAN_POINT('',(-0.0133104533185637,0.0230543814195261,0.087943968307788));
#32905=CARTESIAN_POINT('',(-0.0113660779370141,0.0241769670694694,0.0880762599744547));
#32906=CARTESIAN_POINT('',(-0.0102434922870708,0.026121342451019,0.0882085516411213));
#32907=CARTESIAN_POINT('',(-0.00912090663712744,0.0280657178325686,0.088340843307788));
#32908=CARTESIAN_POINT('',(-0.00912090663712744,0.0303108891324553,0.0884731349744546));
#32909=CARTESIAN_POINT('',(-0.00912090663712744,0.032556060432342,0.0886054266411213));
#32910=CARTESIAN_POINT('',(-0.0102434922870708,0.0345004358138917,0.0887377183077879));
#32911=CARTESIAN_POINT('',(-0.0113660779370141,0.0364448111954412,0.0888700099744546));
#32912=CARTESIAN_POINT('',(-0.0133104533185637,0.0375673968453846,0.0890023016411213));
#32913=CARTESIAN_POINT('',(-0.0152548287001133,0.038689982495328,0.0891345933077879));
#32914=CARTESIAN_POINT('',(-0.0175,0.038689982495328,0.0892668849744546));
#32915=CARTESIAN_POINT('',(-0.0197451712998867,0.038689982495328,0.0893991766411213));
#32916=CARTESIAN_POINT('',(-0.0216895466814364,0.0375673968453846,0.089531468307788));
#32917=CARTESIAN_POINT('',(-0.023633922062986,0.0364448111954412,0.0896637599744546));
#32918=CARTESIAN_POINT('',(-0.0247565077129293,0.0345004358138917,0.0897960516411213));
#32919=CARTESIAN_POINT('',(-0.0258790933628727,0.0325560604323421,0.089928343307788));
#32920=CARTESIAN_POINT('',(-0.0258790933628727,0.0303108891324553,0.0900606349744546));
#32921=CARTESIAN_POINT('',(-0.0258790933628727,0.0280657178325686,0.0901929266411213));
#32922=CARTESIAN_POINT('',(-0.0247565077129293,0.0261213424510191,0.0903252183077879));
#32923=CARTESIAN_POINT('',(-0.023633922062986,0.0241769670694694,0.0904575099744546));
#32924=CARTESIAN_POINT('',(-0.0216895466814364,0.0230543814195261,0.0905898016411213));
#32925=CARTESIAN_POINT('',(-0.0197451712998867,0.0219317957695827,0.0907220933077879));
#32926=CARTESIAN_POINT('',(-0.0175,0.0219317957695827,0.0908543849744546));
#32927=CARTESIAN_POINT('',(-0.0152548287001134,0.0219317957695827,0.0909866766411213));
#32928=CARTESIAN_POINT('',(-0.0133104533185637,0.0230543814195261,0.0911189683077879));
#32929=CARTESIAN_POINT('',(-0.0113660779370141,0.0241769670694694,0.0912512599744547));
#32930=CARTESIAN_POINT('',(-0.0102434922870708,0.026121342451019,0.0913835516411213));
#32931=CARTESIAN_POINT('',(-0.00912090663712744,0.0280657178325686,0.091515843307788));
#32932=CARTESIAN_POINT('',(-0.00912090663712744,0.0303108891324553,0.0916481349744546));
#32933=CARTESIAN_POINT('',(-0.00912090663712743,0.0307461291971821,0.091673780515873));
#32934=CARTESIAN_POINT('',(-0.00916600081685451,0.0311790269090008,0.0917));
#32935=CARTESIAN_POINT('',(-0.00916600081685452,0.0311790269090009,0.0917));
#32936=CARTESIAN_POINT('',(-0.00916600081685452,0.0311790269090008,0.0917));
#32937=CARTESIAN_POINT('',(-0.00923799565048493,0.0313347702922195,0.0917));
#32938=CARTESIAN_POINT('',(-0.00931002513253627,0.0316684151962386,0.0916999999999999));
#32939=CARTESIAN_POINT('',(-0.0095023502836293,0.0323207574022983,0.0917000000000003));
#32940=CARTESIAN_POINT('',(-0.00977549559735775,0.0331234551269965,0.0916999999999976));
#32941=CARTESIAN_POINT('',(-0.0102085406903454,0.034051613931461,0.0917000000000007));
#32942=CARTESIAN_POINT('',(-0.0105596013841118,0.0346332630059237,0.0917));
#32943=CARTESIAN_POINT('',(-0.0107517314949501,0.0349148766241576,0.0917));
#32944=CARTESIAN_POINT('',(-0.00912090663712744,0.0303108891324553,0.0852981349744546));
#32945=CARTESIAN_POINT('',(-0.00912090663712744,0.032556060432342,0.0854304266411213));
#32946=CARTESIAN_POINT('',(-0.0102434922870708,0.0345004358138917,0.0855627183077879));
#32947=CARTESIAN_POINT('',(-0.0113660779370141,0.0364448111954412,0.0856950099744546));
#32948=CARTESIAN_POINT('',(-0.0133104533185637,0.0375673968453846,0.0858273016411213));
#32949=CARTESIAN_POINT('',(-0.0152548287001133,0.038689982495328,0.0859595933077879));
#32950=CARTESIAN_POINT('',(-0.0175,0.038689982495328,0.0860918849744546));
#32951=CARTESIAN_POINT('',(-0.0197451712998867,0.038689982495328,0.0862241766411214));
#32952=CARTESIAN_POINT('',(-0.0216895466814364,0.0375673968453846,0.0863564683077879));
#32953=CARTESIAN_POINT('',(-0.023633922062986,0.0364448111954412,0.0864887599744547));
#32954=CARTESIAN_POINT('',(-0.0247565077129293,0.0345004358138917,0.0866210516411213));
#32955=CARTESIAN_POINT('',(-0.0258790933628727,0.0325560604323421,0.086753343307788));
#32956=CARTESIAN_POINT('',(-0.0258790933628727,0.0303108891324553,0.0868856349744546));
#32957=CARTESIAN_POINT('',(-0.0258790933628727,0.0280657178325686,0.0870179266411213));
#32958=CARTESIAN_POINT('',(-0.0247565077129293,0.0261213424510191,0.087150218307788));
#32959=CARTESIAN_POINT('',(-0.023633922062986,0.0241769670694694,0.0872825099744546));
#32960=CARTESIAN_POINT('',(-0.0216895466814364,0.0230543814195261,0.0874148016411213));
#32961=CARTESIAN_POINT('',(-0.0197451712998867,0.0219317957695827,0.087547093307788));
#32962=CARTESIAN_POINT('',(-0.0175,0.0219317957695827,0.0876793849744546));
#32963=CARTESIAN_POINT('',(-0.0152548287001134,0.0219317957695827,0.0878116766411214));
#32964=CARTESIAN_POINT('',(-0.0133104533185637,0.0230543814195261,0.087943968307788));
#32965=CARTESIAN_POINT('',(-0.0113660779370141,0.0241769670694694,0.0880762599744547));
#32966=CARTESIAN_POINT('',(-0.0102434922870708,0.0261213424510191,0.0882085516411213));
#32967=CARTESIAN_POINT('',(-0.00912090663712744,0.0280657178325686,0.088340843307788));
#32968=CARTESIAN_POINT('',(-0.00912090663712744,0.0303108891324553,0.0884731349744546));
#32969=CARTESIAN_POINT('',(-0.00912090663712744,0.032556060432342,0.0886054266411213));
#32970=CARTESIAN_POINT('',(-0.0102434922870708,0.0345004358138917,0.0887377183077879));
#32971=CARTESIAN_POINT('',(-0.0113660779370141,0.0364448111954412,0.0888700099744546));
#32972=CARTESIAN_POINT('',(-0.0133104533185637,0.0375673968453846,0.0890023016411213));
#32973=CARTESIAN_POINT('',(-0.0152548287001133,0.038689982495328,0.0891345933077879));
#32974=CARTESIAN_POINT('',(-0.0175,0.038689982495328,0.0892668849744546));
#32975=CARTESIAN_POINT('',(-0.0197451712998867,0.038689982495328,0.0893991766411213));
#32976=CARTESIAN_POINT('',(-0.0216895466814364,0.0375673968453846,0.089531468307788));
#32977=CARTESIAN_POINT('',(-0.023633922062986,0.0364448111954412,0.0896637599744546));
#32978=CARTESIAN_POINT('',(-0.0247565077129293,0.0345004358138917,0.0897960516411213));
#32979=CARTESIAN_POINT('',(-0.0258790933628727,0.0325560604323421,0.089928343307788));
#32980=CARTESIAN_POINT('',(-0.0258790933628727,0.0303108891324553,0.0900606349744546));
#32981=CARTESIAN_POINT('',(-0.0258790933628727,0.0280657178325686,0.0901929266411213));
#32982=CARTESIAN_POINT('',(-0.0247565077129293,0.0261213424510191,0.0903252183077879));
#32983=CARTESIAN_POINT('',(-0.023633922062986,0.0241769670694694,0.0904575099744546));
#32984=CARTESIAN_POINT('',(-0.0216895466814364,0.0230543814195261,0.0905898016411213));
#32985=CARTESIAN_POINT('',(-0.0197451712998867,0.0219317957695827,0.0907220933077879));
#32986=CARTESIAN_POINT('',(-0.0175,0.0219317957695827,0.0908543849744546));
#32987=CARTESIAN_POINT('',(-0.0152548287001134,0.0219317957695827,0.0909866766411213));
#32988=CARTESIAN_POINT('',(-0.0133104533185637,0.0230543814195261,0.0911189683077879));
#32989=CARTESIAN_POINT('',(-0.0113660779370141,0.0241769670694694,0.0912512599744547));
#32990=CARTESIAN_POINT('',(-0.0102434922870708,0.0261213424510191,0.0913835516411213));
#32991=CARTESIAN_POINT('',(-0.00912090663712744,0.0280657178325686,0.091515843307788));
#32992=CARTESIAN_POINT('',(-0.00912090663712744,0.0303108891324553,0.0916481349744546));
#32993=CARTESIAN_POINT('',(-0.00912090663712744,0.0310669305934274,0.091692683016266));
#32994=CARTESIAN_POINT('',(-0.00925623934052464,0.0318107610513275,0.091738648225955));
#32995=CARTESIAN_POINT('',(-0.00847389336287264,0.0303108891324553,0.0854122208715823));
#32996=CARTESIAN_POINT('',(-0.00847389336287265,0.0327294271166708,0.085544512538249));
#32997=CARTESIAN_POINT('',(-0.00968316235498038,0.0348239424510191,0.0856768042049156));
#32998=CARTESIAN_POINT('',(-0.0108924313470881,0.0369184577853673,0.0858090958715823));
#32999=CARTESIAN_POINT('',(-0.0129869466814363,0.038127726777475,0.0859413875382489));
#33000=CARTESIAN_POINT('',(-0.0150814620157846,0.0393369957695828,0.0860736792049156));
#33001=CARTESIAN_POINT('',(-0.0175,0.0393369957695828,0.0862059708715822));
#33002=CARTESIAN_POINT('',(-0.0199185379842156,0.0393369957695828,0.086338262538249));
#33003=CARTESIAN_POINT('',(-0.0220130533185638,0.038127726777475,0.0864705542049156));
#33004=CARTESIAN_POINT('',(-0.024107568652912,0.0369184577853673,0.0866028458715823));
#33005=CARTESIAN_POINT('',(-0.0253168376450197,0.0348239424510191,0.0867351375382489));
#33006=CARTESIAN_POINT('',(-0.0265261066371274,0.0327294271166708,0.0868674292049156));
#33007=CARTESIAN_POINT('',(-0.0265261066371274,0.0303108891324553,0.0869997208715823));
#33008=CARTESIAN_POINT('',(-0.0265261066371274,0.0278923511482398,0.0871320125382489));
#33009=CARTESIAN_POINT('',(-0.0253168376450197,0.0257978358138917,0.0872643042049156));
#33010=CARTESIAN_POINT('',(-0.024107568652912,0.0237033204795434,0.0873965958715823));
#33011=CARTESIAN_POINT('',(-0.0220130533185638,0.0224940514874357,0.0875288875382489));
#33012=CARTESIAN_POINT('',(-0.0199185379842156,0.021284782495328,0.0876611792049156));
#33013=CARTESIAN_POINT('',(-0.0175,0.021284782495328,0.0877934708715823));
#33014=CARTESIAN_POINT('',(-0.0150814620157846,0.0212847824953279,0.087925762538249));
#33015=CARTESIAN_POINT('',(-0.0129869466814363,0.0224940514874356,0.0880580542049156));
#33016=CARTESIAN_POINT('',(-0.0108924313470881,0.0237033204795434,0.0881903458715823));
#33017=CARTESIAN_POINT('',(-0.00968316235498039,0.0257978358138917,0.0883226375382489));
#33018=CARTESIAN_POINT('',(-0.00847389336287265,0.0278923511482398,0.0884549292049156));
#33019=CARTESIAN_POINT('',(-0.00847389336287264,0.0303108891324553,0.0885872208715823));
#33020=CARTESIAN_POINT('',(-0.00847389336287265,0.0327294271166708,0.0887195125382489));
#33021=CARTESIAN_POINT('',(-0.00968316235498038,0.0348239424510191,0.0888518042049156));
#33022=CARTESIAN_POINT('',(-0.0108924313470881,0.0369184577853673,0.0889840958715822));
#33023=CARTESIAN_POINT('',(-0.0129869466814363,0.038127726777475,0.0891163875382489));
#33024=CARTESIAN_POINT('',(-0.0150814620157846,0.0393369957695828,0.0892486792049156));
#33025=CARTESIAN_POINT('',(-0.0175,0.0393369957695828,0.0893809708715822));
#33026=CARTESIAN_POINT('',(-0.0199185379842156,0.0393369957695828,0.089513262538249));
#33027=CARTESIAN_POINT('',(-0.0220130533185638,0.038127726777475,0.0896455542049156));
#33028=CARTESIAN_POINT('',(-0.024107568652912,0.0369184577853673,0.0897778458715823));
#33029=CARTESIAN_POINT('',(-0.0253168376450197,0.0348239424510191,0.0899101375382489));
#33030=CARTESIAN_POINT('',(-0.0265261066371274,0.0327294271166708,0.0900424292049156));
#33031=CARTESIAN_POINT('',(-0.0265261066371274,0.0303108891324553,0.0901747208715823));
#33032=CARTESIAN_POINT('',(-0.0265261066371274,0.0278923511482398,0.0903070125382489));
#33033=CARTESIAN_POINT('',(-0.0253168376450197,0.0257978358138917,0.0904393042049156));
#33034=CARTESIAN_POINT('',(-0.024107568652912,0.0237033204795434,0.0905715958715823));
#33035=CARTESIAN_POINT('',(-0.0220130533185638,0.0224940514874357,0.0907038875382489));
#33036=CARTESIAN_POINT('',(-0.0199185379842156,0.021284782495328,0.0908361792049157));
#33037=CARTESIAN_POINT('',(-0.0175,0.021284782495328,0.0909684708715822));
#33038=CARTESIAN_POINT('',(-0.0150814620157846,0.0212847824953279,0.091100762538249));
#33039=CARTESIAN_POINT('',(-0.0129869466814363,0.0224940514874356,0.0912330542049156));
#33040=CARTESIAN_POINT('',(-0.0108924313470881,0.0237033204795434,0.0913653458715823));
#33041=CARTESIAN_POINT('',(-0.00968316235498039,0.0257978358138917,0.0914976375382489));
#33042=CARTESIAN_POINT('',(-0.00847389336287265,0.0278923511482398,0.0916299292049156));
#33043=CARTESIAN_POINT('',(-0.00847389336287264,0.0303108891324553,0.0917622208715822));
#33044=CARTESIAN_POINT('',(-0.00847389336287264,0.0311253102820108,0.0918067689133936));
#33045=CARTESIAN_POINT('',(-0.00861967612951019,0.0319265775244429,0.0918527341230826));
#33046=CARTESIAN_POINT('',(-0.00847389336287264,0.0303108891324553,0.0854122208715823));
#33047=CARTESIAN_POINT('',(-0.00847389336287265,0.0327294271166708,0.085544512538249));
#33048=CARTESIAN_POINT('',(-0.00968316235498038,0.0348239424510191,0.0856768042049156));
#33049=CARTESIAN_POINT('',(-0.0108924313470881,0.0369184577853673,0.0858090958715823));
#33050=CARTESIAN_POINT('',(-0.0129869466814363,0.038127726777475,0.0859413875382489));
#33051=CARTESIAN_POINT('',(-0.0150814620157846,0.0393369957695828,0.0860736792049156));
#33052=CARTESIAN_POINT('',(-0.0175,0.0393369957695828,0.0862059708715822));
#33053=CARTESIAN_POINT('',(-0.0199185379842156,0.0393369957695828,0.086338262538249));
#33054=CARTESIAN_POINT('',(-0.0220130533185638,0.038127726777475,0.0864705542049156));
#33055=CARTESIAN_POINT('',(-0.024107568652912,0.0369184577853673,0.0866028458715823));
#33056=CARTESIAN_POINT('',(-0.0253168376450197,0.0348239424510191,0.0867351375382489));
#33057=CARTESIAN_POINT('',(-0.0265261066371274,0.0327294271166708,0.0868674292049156));
#33058=CARTESIAN_POINT('',(-0.0265261066371274,0.0303108891324553,0.0869997208715823));
#33059=CARTESIAN_POINT('',(-0.0265261066371274,0.0278923511482398,0.0871320125382489));
#33060=CARTESIAN_POINT('',(-0.0253168376450197,0.0257978358138917,0.0872643042049156));
#33061=CARTESIAN_POINT('',(-0.024107568652912,0.0237033204795434,0.0873965958715823));
#33062=CARTESIAN_POINT('',(-0.0220130533185638,0.0224940514874357,0.0875288875382489));
#33063=CARTESIAN_POINT('',(-0.0199185379842156,0.021284782495328,0.0876611792049155));
#33064=CARTESIAN_POINT('',(-0.0175,0.021284782495328,0.0877934708715823));
#33065=CARTESIAN_POINT('',(-0.0150814620157846,0.021284782495328,0.087925762538249));
#33066=CARTESIAN_POINT('',(-0.0129869466814363,0.0224940514874356,0.0880580542049156));
#33067=CARTESIAN_POINT('',(-0.0108924313470881,0.0237033204795434,0.0881903458715823));
#33068=CARTESIAN_POINT('',(-0.00968316235498039,0.0257978358138917,0.0883226375382489));
#33069=CARTESIAN_POINT('',(-0.00847389336287265,0.0278923511482398,0.0884549292049156));
#33070=CARTESIAN_POINT('',(-0.00847389336287264,0.0303108891324553,0.0885872208715823));
#33071=CARTESIAN_POINT('',(-0.00847389336287265,0.0327294271166708,0.088719512538249));
#33072=CARTESIAN_POINT('',(-0.00968316235498038,0.0348239424510191,0.0888518042049156));
#33073=CARTESIAN_POINT('',(-0.0108924313470881,0.0369184577853673,0.0889840958715823));
#33074=CARTESIAN_POINT('',(-0.0129869466814363,0.038127726777475,0.0891163875382489));
#33075=CARTESIAN_POINT('',(-0.0150814620157846,0.0393369957695828,0.0892486792049156));
#33076=CARTESIAN_POINT('',(-0.0175,0.0393369957695828,0.0893809708715822));
#33077=CARTESIAN_POINT('',(-0.0199185379842156,0.0393369957695828,0.089513262538249));
#33078=CARTESIAN_POINT('',(-0.0220130533185638,0.038127726777475,0.0896455542049156));
#33079=CARTESIAN_POINT('',(-0.024107568652912,0.0369184577853673,0.0897778458715823));
#33080=CARTESIAN_POINT('',(-0.0253168376450197,0.0348239424510191,0.0899101375382489));
#33081=CARTESIAN_POINT('',(-0.0265261066371274,0.0327294271166708,0.0900424292049156));
#33082=CARTESIAN_POINT('',(-0.0265261066371274,0.0303108891324553,0.0901747208715823));
#33083=CARTESIAN_POINT('',(-0.0265261066371274,0.0278923511482398,0.0903070125382489));
#33084=CARTESIAN_POINT('',(-0.0253168376450197,0.0257978358138917,0.0904393042049156));
#33085=CARTESIAN_POINT('',(-0.024107568652912,0.0237033204795434,0.0905715958715823));
#33086=CARTESIAN_POINT('',(-0.0220130533185638,0.0224940514874357,0.0907038875382489));
#33087=CARTESIAN_POINT('',(-0.0199185379842156,0.021284782495328,0.0908361792049157));
#33088=CARTESIAN_POINT('',(-0.0175,0.021284782495328,0.0909684708715822));
#33089=CARTESIAN_POINT('',(-0.0150814620157846,0.021284782495328,0.091100762538249));
#33090=CARTESIAN_POINT('',(-0.0129869466814363,0.0224940514874356,0.0912330542049156));
#33091=CARTESIAN_POINT('',(-0.0108924313470881,0.0237033204795434,0.0913653458715823));
#33092=CARTESIAN_POINT('',(-0.00968316235498039,0.0257978358138917,0.0914976375382489));
#33093=CARTESIAN_POINT('',(-0.00876991648182173,0.027379624066005,0.091597544853681));
#33094=CARTESIAN_POINT('',(-0.00854350778716387,0.0291920288779395,0.0917000000000564));
#33095=CARTESIAN_POINT('',(-0.0085435077872263,0.0291920288774397,0.0917000000000283));
#33096=CARTESIAN_POINT('',(-0.00854350778722381,0.0291920288774402,0.0917));
#33097=CARTESIAN_POINT('',(-0.00867070228446611,0.0298765386535114,0.0917));
#33098=CARTESIAN_POINT('',(-0.008873827876199,0.0305469815250745,0.0917));
#33099=CARTESIAN_POINT('',(-0.00916600081685446,0.0311790269090009,0.0917));
#33100=CARTESIAN_POINT('',(-0.00847389336287264,0.0303108891324553,0.0854122208715823));
#33101=CARTESIAN_POINT('',(-0.00847389336287265,0.0327294271166708,0.085544512538249));
#33102=CARTESIAN_POINT('',(-0.00968316235498038,0.0348239424510191,0.0856768042049156));
#33103=CARTESIAN_POINT('',(-0.0108924313470881,0.0369184577853673,0.0858090958715823));
#33104=CARTESIAN_POINT('',(-0.0129869466814363,0.038127726777475,0.0859413875382489));
#33105=CARTESIAN_POINT('',(-0.0150814620157846,0.0393369957695828,0.0860736792049156));
#33106=CARTESIAN_POINT('',(-0.0175,0.0393369957695828,0.0862059708715822));
#33107=CARTESIAN_POINT('',(-0.0199185379842156,0.0393369957695828,0.086338262538249));
#33108=CARTESIAN_POINT('',(-0.0220130533185638,0.038127726777475,0.0864705542049156));
#33109=CARTESIAN_POINT('',(-0.024107568652912,0.0369184577853673,0.0866028458715823));
#33110=CARTESIAN_POINT('',(-0.0253168376450197,0.0348239424510191,0.0867351375382489));
#33111=CARTESIAN_POINT('',(-0.0265261066371274,0.0327294271166708,0.0868674292049156));
#33112=CARTESIAN_POINT('',(-0.0265261066371274,0.0303108891324553,0.0869997208715823));
#33113=CARTESIAN_POINT('',(-0.0265261066371274,0.0278923511482399,0.0871320125382489));
#33114=CARTESIAN_POINT('',(-0.0253168376450197,0.0257978358138917,0.0872643042049156));
#33115=CARTESIAN_POINT('',(-0.024107568652912,0.0237033204795435,0.0873965958715823));
#33116=CARTESIAN_POINT('',(-0.0220130533185638,0.0224940514874357,0.0875288875382489));
#33117=CARTESIAN_POINT('',(-0.0199185379842156,0.021284782495328,0.0876611792049156));
#33118=CARTESIAN_POINT('',(-0.0175,0.021284782495328,0.0877934708715823));
#33119=CARTESIAN_POINT('',(-0.0150814620157846,0.0212847824953279,0.087925762538249));
#33120=CARTESIAN_POINT('',(-0.0129869466814364,0.0224940514874356,0.0880580542049156));
#33121=CARTESIAN_POINT('',(-0.0108924313470881,0.0237033204795434,0.0881903458715823));
#33122=CARTESIAN_POINT('',(-0.00968316235498039,0.0257978358138917,0.0883226375382489));
#33123=CARTESIAN_POINT('',(-0.00847389336287265,0.0278923511482398,0.0884549292049156));
#33124=CARTESIAN_POINT('',(-0.00847389336287264,0.0303108891324553,0.0885872208715823));
#33125=CARTESIAN_POINT('',(-0.00847389336287265,0.0327294271166708,0.0887195125382489));
#33126=CARTESIAN_POINT('',(-0.00968316235498038,0.0348239424510191,0.0888518042049156));
#33127=CARTESIAN_POINT('',(-0.0108924313470881,0.0369184577853673,0.0889840958715822));
#33128=CARTESIAN_POINT('',(-0.0129869466814363,0.038127726777475,0.0891163875382489));
#33129=CARTESIAN_POINT('',(-0.0150814620157846,0.0393369957695828,0.0892486792049156));
#33130=CARTESIAN_POINT('',(-0.0175,0.0393369957695828,0.0893809708715822));
#33131=CARTESIAN_POINT('',(-0.0199185379842156,0.0393369957695828,0.089513262538249));
#33132=CARTESIAN_POINT('',(-0.0220130533185638,0.038127726777475,0.0896455542049156));
#33133=CARTESIAN_POINT('',(-0.024107568652912,0.0369184577853673,0.0897778458715823));
#33134=CARTESIAN_POINT('',(-0.0253168376450197,0.0348239424510191,0.0899101375382489));
#33135=CARTESIAN_POINT('',(-0.0265261066371274,0.0327294271166708,0.0900424292049156));
#33136=CARTESIAN_POINT('',(-0.0265261066371274,0.0303108891324553,0.0901747208715823));
#33137=CARTESIAN_POINT('',(-0.0265261066371274,0.0278923511482399,0.0903070125382489));
#33138=CARTESIAN_POINT('',(-0.0253168376450197,0.0257978358138917,0.0904393042049156));
#33139=CARTESIAN_POINT('',(-0.024107568652912,0.0237033204795435,0.0905715958715823));
#33140=CARTESIAN_POINT('',(-0.0220130533185638,0.0224940514874357,0.0907038875382489));
#33141=CARTESIAN_POINT('',(-0.0199185379842156,0.021284782495328,0.0908361792049157));
#33142=CARTESIAN_POINT('',(-0.0175,0.021284782495328,0.0909684708715822));
#33143=CARTESIAN_POINT('',(-0.0150814620157846,0.0212847824953279,0.091100762538249));
#33144=CARTESIAN_POINT('',(-0.0129869466814364,0.0224940514874356,0.0912330542049156));
#33145=CARTESIAN_POINT('',(-0.0108924313470881,0.0237033204795434,0.0913653458715823));
#33146=CARTESIAN_POINT('',(-0.00968316235498039,0.0257978358138917,0.0914976375382489));
#33147=CARTESIAN_POINT('',(-0.00859351540386823,0.0276851596955304,0.09161684278719));
#33148=CARTESIAN_POINT('',(-0.00848507467546628,0.0298617539435922,0.091737489735644));
#33149=CARTESIAN_POINT('',(-0.00834689336287265,0.0303108891324553,0.0854346143981323));
#33150=CARTESIAN_POINT('',(-0.00834689336287264,0.0327634566641096,0.0855669060647989));
#33151=CARTESIAN_POINT('',(-0.00957317712869975,0.0348874424510191,0.0856991977314656));
#33152=CARTESIAN_POINT('',(-0.0107994608945269,0.0370114282379285,0.0858314893981323));
#33153=CARTESIAN_POINT('',(-0.0129234466814363,0.0382377120037556,0.0859637810647989));
#33154=CARTESIAN_POINT('',(-0.0150474324683458,0.0394639957695828,0.0860960727314655));
#33155=CARTESIAN_POINT('',(-0.0175,0.0394639957695827,0.0862283643981323));
#33156=CARTESIAN_POINT('',(-0.0199525675316543,0.0394639957695828,0.0863606560647989));
#33157=CARTESIAN_POINT('',(-0.0220765533185638,0.0382377120037556,0.0864929477314656));
#33158=CARTESIAN_POINT('',(-0.0242005391054732,0.0370114282379285,0.0866252393981323));
#33159=CARTESIAN_POINT('',(-0.0254268228713003,0.0348874424510191,0.0867575310647989));
#33160=CARTESIAN_POINT('',(-0.0266531066371274,0.0327634566641096,0.0868898227314656));
#33161=CARTESIAN_POINT('',(-0.0266531066371274,0.0303108891324553,0.0870221143981322));
#33162=CARTESIAN_POINT('',(-0.0266531066371274,0.0278583216008011,0.087154406064799));
#33163=CARTESIAN_POINT('',(-0.0254268228713003,0.0257343358138916,0.0872866977314655));
#33164=CARTESIAN_POINT('',(-0.0242005391054732,0.0236103500269822,0.0874189893981322));
#33165=CARTESIAN_POINT('',(-0.0220765533185638,0.022384066261155,0.0875512810647989));
#33166=CARTESIAN_POINT('',(-0.0199525675316543,0.021157782495328,0.0876835727314656));
#33167=CARTESIAN_POINT('',(-0.0175,0.0211577824953279,0.0878158643981322));
#33168=CARTESIAN_POINT('',(-0.0150474324683458,0.021157782495328,0.0879481560647989));
#33169=CARTESIAN_POINT('',(-0.0129234466814363,0.022384066261155,0.0880804477314655));
#33170=CARTESIAN_POINT('',(-0.0107994608945269,0.0236103500269822,0.0882127393981323));
#33171=CARTESIAN_POINT('',(-0.00957317712869976,0.0257343358138916,0.0883450310647989));
#33172=CARTESIAN_POINT('',(-0.00834689336287266,0.0278583216008011,0.0884773227314656));
#33173=CARTESIAN_POINT('',(-0.00834689336287265,0.0303108891324553,0.0886096143981323));
#33174=CARTESIAN_POINT('',(-0.00834689336287264,0.0327634566641096,0.088741906064799));
#33175=CARTESIAN_POINT('',(-0.00957317712869975,0.0348874424510191,0.0888741977314656));
#33176=CARTESIAN_POINT('',(-0.0107994608945269,0.0370114282379285,0.0890064893981322));
#33177=CARTESIAN_POINT('',(-0.0129234466814363,0.0382377120037556,0.0891387810647989));
#33178=CARTESIAN_POINT('',(-0.0150474324683458,0.0394639957695828,0.0892710727314656));
#33179=CARTESIAN_POINT('',(-0.0175,0.0394639957695827,0.0894033643981323));
#33180=CARTESIAN_POINT('',(-0.0199525675316543,0.0394639957695828,0.0895356560647989));
#33181=CARTESIAN_POINT('',(-0.0220765533185638,0.0382377120037556,0.0896679477314656));
#33182=CARTESIAN_POINT('',(-0.0242005391054732,0.0370114282379285,0.0898002393981323));
#33183=CARTESIAN_POINT('',(-0.0254268228713003,0.0348874424510191,0.0899325310647989));
#33184=CARTESIAN_POINT('',(-0.0266531066371274,0.0327634566641096,0.0900648227314657));
#33185=CARTESIAN_POINT('',(-0.0266531066371274,0.0303108891324553,0.0901971143981322));
#33186=CARTESIAN_POINT('',(-0.0266531066371274,0.0278583216008011,0.0903294060647989));
#33187=CARTESIAN_POINT('',(-0.0254268228713003,0.0257343358138916,0.0904616977314656));
#33188=CARTESIAN_POINT('',(-0.0242005391054732,0.0236103500269822,0.0905939893981322));
#33189=CARTESIAN_POINT('',(-0.0220765533185638,0.022384066261155,0.0907262810647989));
#33190=CARTESIAN_POINT('',(-0.0199525675316543,0.021157782495328,0.0908585727314656));
#33191=CARTESIAN_POINT('',(-0.0175,0.0211577824953279,0.0909908643981322));
#33192=CARTESIAN_POINT('',(-0.0150474324683458,0.021157782495328,0.091123156064799));
#33193=CARTESIAN_POINT('',(-0.0129234466814363,0.022384066261155,0.0912554477314655));
#33194=CARTESIAN_POINT('',(-0.0107994608945269,0.0236103500269822,0.0913877393981323));
#33195=CARTESIAN_POINT('',(-0.00957317712869976,0.0257343358138916,0.0915200310647988));
#33196=CARTESIAN_POINT('',(-0.00846819852149771,0.0276482149028423,0.09163923631374));
#33197=CARTESIAN_POINT('',(-0.00835823199985392,0.0298554344781484,0.091759883262194));
#33198=CARTESIAN_POINT('',(-0.00826400000000004,0.0303108891324553,0.0855334028611379));
#33199=CARTESIAN_POINT('',(-0.00826400000000004,0.0327856678737492,0.0856656945278046));
#33200=CARTESIAN_POINT('',(-0.00950138937064697,0.0349288891324553,0.0857979861944712));
#33201=CARTESIAN_POINT('',(-0.0107387787412939,0.0370721103911615,0.0859302778611379));
#33202=CARTESIAN_POINT('',(-0.012882,0.0383094997618084,0.0860625695278045));
#33203=CARTESIAN_POINT('',(-0.0150252212587062,0.0395468891324554,0.0861948611944711));
#33204=CARTESIAN_POINT('',(-0.0175,0.0395468891324554,0.0863271528611379));
#33205=CARTESIAN_POINT('',(-0.0199747787412939,0.0395468891324554,0.0864594445278045));
#33206=CARTESIAN_POINT('',(-0.022118,0.0383094997618084,0.0865917361944712));
#33207=CARTESIAN_POINT('',(-0.0242612212587062,0.0370721103911615,0.0867240278611378));
#33208=CARTESIAN_POINT('',(-0.0254986106293532,0.0349288891324553,0.0868563195278045));
#33209=CARTESIAN_POINT('',(-0.0267360000000001,0.0327856678737492,0.0869886111944712));
#33210=CARTESIAN_POINT('',(-0.0267360000000001,0.0303108891324553,0.0871209028611378));
#33211=CARTESIAN_POINT('',(-0.0267360000000001,0.0278361103911615,0.0872531945278046));
#33212=CARTESIAN_POINT('',(-0.0254986106293532,0.0256928891324553,0.0873854861944711));
#33213=CARTESIAN_POINT('',(-0.0242612212587062,0.0235496678737492,0.0875177778611379));
#33214=CARTESIAN_POINT('',(-0.022118,0.0223122785031023,0.0876500695278045));
#33215=CARTESIAN_POINT('',(-0.0199747787412939,0.0210748891324553,0.0877823611944713));
#33216=CARTESIAN_POINT('',(-0.0175,0.0210748891324553,0.0879146528611379));
#33217=CARTESIAN_POINT('',(-0.0150252212587062,0.0210748891324553,0.0880469445278045));
#33218=CARTESIAN_POINT('',(-0.012882,0.0223122785031023,0.0881792361944712));
#33219=CARTESIAN_POINT('',(-0.0107387787412939,0.0235496678737492,0.0883115278611379));
#33220=CARTESIAN_POINT('',(-0.00950138937064697,0.0256928891324553,0.0884438195278046));
#33221=CARTESIAN_POINT('',(-0.00826400000000005,0.0278361103911615,0.0885761111944712));
#33222=CARTESIAN_POINT('',(-0.00826400000000004,0.0303108891324553,0.0887084028611379));
#33223=CARTESIAN_POINT('',(-0.00826400000000004,0.0327856678737492,0.0888406945278046));
#33224=CARTESIAN_POINT('',(-0.00950138937064697,0.0349288891324553,0.0889729861944712));
#33225=CARTESIAN_POINT('',(-0.0107387787412939,0.0370721103911615,0.0891052778611379));
#33226=CARTESIAN_POINT('',(-0.012882,0.0383094997618084,0.0892375695278045));
#33227=CARTESIAN_POINT('',(-0.0150252212587062,0.0395468891324554,0.0893698611944712));
#33228=CARTESIAN_POINT('',(-0.0175,0.0395468891324554,0.0895021528611379));
#33229=CARTESIAN_POINT('',(-0.0199747787412939,0.0395468891324554,0.0896344445278045));
#33230=CARTESIAN_POINT('',(-0.022118,0.0383094997618084,0.0897667361944712));
#33231=CARTESIAN_POINT('',(-0.0242612212587062,0.0370721103911615,0.0898990278611379));
#33232=CARTESIAN_POINT('',(-0.0254986106293532,0.0349288891324553,0.0900313195278045));
#33233=CARTESIAN_POINT('',(-0.0267360000000001,0.0327856678737492,0.0901636111944712));
#33234=CARTESIAN_POINT('',(-0.0267360000000001,0.0303108891324553,0.0902959028611378));
#33235=CARTESIAN_POINT('',(-0.0267360000000001,0.0278361103911615,0.0904281945278046));
#33236=CARTESIAN_POINT('',(-0.0254986106293532,0.0256928891324553,0.0905604861944712));
#33237=CARTESIAN_POINT('',(-0.0242612212587062,0.0235496678737492,0.0906927778611378));
#33238=CARTESIAN_POINT('',(-0.022118,0.0223122785031023,0.0908250695278045));
#33239=CARTESIAN_POINT('',(-0.0199747787412939,0.0210748891324553,0.0909573611944712));
#33240=CARTESIAN_POINT('',(-0.0175,0.0210748891324553,0.0910896528611378));
#33241=CARTESIAN_POINT('',(-0.0150252212587062,0.0210748891324553,0.0912219445278045));
#33242=CARTESIAN_POINT('',(-0.012882,0.0223122785031023,0.0913542361944712));
#33243=CARTESIAN_POINT('',(-0.0107387787412939,0.0235496678737492,0.0914865278611379));
#33244=CARTESIAN_POINT('',(-0.00950138937064697,0.0256928891324553,0.0916188195278046));
#33245=CARTESIAN_POINT('',(-0.00838640373563626,0.0276241009020033,0.0917380247767456));
#33246=CARTESIAN_POINT('',(-0.00827544132318252,0.0298513097400209,0.0918586717251997));
#33247=CARTESIAN_POINT('',(-0.008264,0.0303108891324553,0.0856623620408474));
#33248=CARTESIAN_POINT('',(-0.00826400000000004,0.0327856678737492,0.0857946537075141));
#33249=CARTESIAN_POINT('',(-0.00950138937064697,0.0349288891324553,0.0859269453741807));
#33250=CARTESIAN_POINT('',(-0.0107387787412939,0.0370721103911615,0.0860592370408474));
#33251=CARTESIAN_POINT('',(-0.012882,0.0383094997618084,0.086191528707514));
#33252=CARTESIAN_POINT('',(-0.0150252212587062,0.0395468891324554,0.0863238203741807));
#33253=CARTESIAN_POINT('',(-0.0175,0.0395468891324554,0.0864561120408473));
#33254=CARTESIAN_POINT('',(-0.0199747787412939,0.0395468891324554,0.086588403707514));
#33255=CARTESIAN_POINT('',(-0.022118,0.0383094997618084,0.0867206953741807));
#33256=CARTESIAN_POINT('',(-0.0242612212587062,0.0370721103911615,0.0868529870408474));
#33257=CARTESIAN_POINT('',(-0.0254986106293531,0.0349288891324553,0.086985278707514));
#33258=CARTESIAN_POINT('',(-0.0267360000000001,0.0327856678737492,0.0871175703741807));
#33259=CARTESIAN_POINT('',(-0.026736,0.0303108891324553,0.0872498620408474));
#33260=CARTESIAN_POINT('',(-0.0267360000000001,0.0278361103911615,0.087382153707514));
#33261=CARTESIAN_POINT('',(-0.0254986106293531,0.0256928891324554,0.0875144453741807));
#33262=CARTESIAN_POINT('',(-0.0242612212587062,0.0235496678737492,0.0876467370408473));
#33263=CARTESIAN_POINT('',(-0.022118,0.0223122785031023,0.087779028707514));
#33264=CARTESIAN_POINT('',(-0.0199747787412939,0.0210748891324554,0.0879113203741807));
#33265=CARTESIAN_POINT('',(-0.0175,0.0210748891324553,0.0880436120408474));
#33266=CARTESIAN_POINT('',(-0.0150252212587062,0.0210748891324553,0.088175903707514));
#33267=CARTESIAN_POINT('',(-0.012882,0.0223122785031023,0.0883081953741807));
#33268=CARTESIAN_POINT('',(-0.0107387787412939,0.0235496678737492,0.0884404870408474));
#33269=CARTESIAN_POINT('',(-0.00950138937064697,0.0256928891324554,0.088572778707514));
#33270=CARTESIAN_POINT('',(-0.00826400000000005,0.0278361103911615,0.0887050703741807));
#33271=CARTESIAN_POINT('',(-0.008264,0.0303108891324553,0.0888373620408473));
#33272=CARTESIAN_POINT('',(-0.00826400000000004,0.0327856678737492,0.088969653707514));
#33273=CARTESIAN_POINT('',(-0.00950138937064697,0.0349288891324553,0.0891019453741807));
#33274=CARTESIAN_POINT('',(-0.0107387787412939,0.0370721103911615,0.0892342370408473));
#33275=CARTESIAN_POINT('',(-0.012882,0.0383094997618084,0.089366528707514));
#33276=CARTESIAN_POINT('',(-0.0150252212587062,0.0395468891324554,0.0894988203741807));
#33277=CARTESIAN_POINT('',(-0.0175,0.0395468891324554,0.0896311120408473));
#33278=CARTESIAN_POINT('',(-0.0199747787412939,0.0395468891324554,0.0897634037075141));
#33279=CARTESIAN_POINT('',(-0.022118,0.0383094997618084,0.0898956953741807));
#33280=CARTESIAN_POINT('',(-0.0242612212587062,0.0370721103911615,0.0900279870408474));
#33281=CARTESIAN_POINT('',(-0.0254986106293531,0.0349288891324553,0.090160278707514));
#33282=CARTESIAN_POINT('',(-0.0267360000000001,0.0327856678737492,0.0902925703741807));
#33283=CARTESIAN_POINT('',(-0.026736,0.0303108891324553,0.0904248620408473));
#33284=CARTESIAN_POINT('',(-0.0267360000000001,0.0278361103911615,0.090557153707514));
#33285=CARTESIAN_POINT('',(-0.0254986106293531,0.0256928891324554,0.0906894453741807));
#33286=CARTESIAN_POINT('',(-0.0242612212587062,0.0235496678737492,0.0908217370408474));
#33287=CARTESIAN_POINT('',(-0.022118,0.0223122785031023,0.090954028707514));
#33288=CARTESIAN_POINT('',(-0.0199747787412939,0.0210748891324554,0.0910863203741807));
#33289=CARTESIAN_POINT('',(-0.0175,0.0210748891324553,0.0912186120408473));
#33290=CARTESIAN_POINT('',(-0.0150252212587062,0.0210748891324553,0.0913509037075141));
#33291=CARTESIAN_POINT('',(-0.012882,0.0223122785031023,0.0914831953741807));
#33292=CARTESIAN_POINT('',(-0.0107387787412939,0.0235496678737492,0.0916154870408474));
#33293=CARTESIAN_POINT('',(-0.00950138937064697,0.0256928891324554,0.091747778707514));
#33294=CARTESIAN_POINT('',(-0.00838640373563626,0.0276241009020033,0.0918669839564551));
#33295=CARTESIAN_POINT('',(-0.00827544132318248,0.0298513097400209,0.0919876309049091));
#33296=CARTESIAN_POINT('',(-0.00997922046889643,0.0249497725281897,0.0917));
#33297=CARTESIAN_POINT('',(-0.00975815321976537,0.0252598941250487,0.0917));
#33298=CARTESIAN_POINT('',(-0.00935880114911267,0.02590976181805,0.0917000000000014));
#33299=CARTESIAN_POINT('',(-0.008904491714687,0.0269479762400238,0.091699999999995));
#33300=CARTESIAN_POINT('',(-0.00864371501392561,0.0278685853564734,0.0917000000000148));
#33301=CARTESIAN_POINT('',(-0.00854235352036947,0.0286227935316649,0.0916999999999744));
#33302=CARTESIAN_POINT('',(-0.00850783637718163,0.0290000596521613,0.0917000000000565));
#33303=CARTESIAN_POINT('',(-0.00854350778706608,0.0291920288774134,0.0917000000000565));
#33304=CARTESIAN_POINT('',(-0.008264,0.0303108891324553,0.0856623620408474));
#33305=CARTESIAN_POINT('',(-0.00826400000000004,0.0327856678737492,0.0857946537075141));
#33306=CARTESIAN_POINT('',(-0.00950138937064697,0.0349288891324553,0.0859269453741807));
#33307=CARTESIAN_POINT('',(-0.0107387787412939,0.0370721103911615,0.0860592370408474));
#33308=CARTESIAN_POINT('',(-0.012882,0.0383094997618084,0.086191528707514));
#33309=CARTESIAN_POINT('',(-0.0150252212587062,0.0395468891324554,0.0863238203741807));
#33310=CARTESIAN_POINT('',(-0.0175,0.0395468891324554,0.0864561120408473));
#33311=CARTESIAN_POINT('',(-0.0199747787412939,0.0395468891324554,0.086588403707514));
#33312=CARTESIAN_POINT('',(-0.022118,0.0383094997618084,0.0867206953741807));
#33313=CARTESIAN_POINT('',(-0.0242612212587062,0.0370721103911615,0.0868529870408474));
#33314=CARTESIAN_POINT('',(-0.0254986106293531,0.0349288891324553,0.086985278707514));
#33315=CARTESIAN_POINT('',(-0.0267360000000001,0.0327856678737491,0.0871175703741807));
#33316=CARTESIAN_POINT('',(-0.026736,0.0303108891324553,0.0872498620408474));
#33317=CARTESIAN_POINT('',(-0.026736,0.0303108891324553,0.0872498620408474));
#33318=CARTESIAN_POINT('',(-0.026736,0.0303108891324553,0.0872498620408473));
#33319=CARTESIAN_POINT('',(-0.0267360000000001,0.0278361103911614,0.087382153707514));
#33320=CARTESIAN_POINT('',(-0.0254986106293531,0.0256928891324554,0.0875144453741807));
#33321=CARTESIAN_POINT('',(-0.0242612212587062,0.0235496678737492,0.0876467370408474));
#33322=CARTESIAN_POINT('',(-0.022118,0.0223122785031023,0.087779028707514));
#33323=CARTESIAN_POINT('',(-0.0199747787412939,0.0210748891324553,0.0879113203741807));
#33324=CARTESIAN_POINT('',(-0.0175,0.0210748891324553,0.0880436120408474));
#33325=CARTESIAN_POINT('',(-0.0150252212587062,0.0210748891324553,0.088175903707514));
#33326=CARTESIAN_POINT('',(-0.012882,0.0223122785031023,0.0883081953741807));
#33327=CARTESIAN_POINT('',(-0.0107387787412939,0.0235496678737492,0.0884404870408474));
#33328=CARTESIAN_POINT('',(-0.00950138937064697,0.0256928891324554,0.088572778707514));
#33329=CARTESIAN_POINT('',(-0.00826400000000006,0.0278361103911614,0.0887050703741806));
#33330=CARTESIAN_POINT('',(-0.008264,0.0303108891324553,0.0888373620408473));
#33331=CARTESIAN_POINT('',(-0.008264,0.0303108891324553,0.0888373620408473));
#33332=CARTESIAN_POINT('',(-0.008264,0.0303108891324553,0.0888373620408474));
#33333=CARTESIAN_POINT('',(-0.00826400000000003,0.0327856678737492,0.088969653707514));
#33334=CARTESIAN_POINT('',(-0.00950138937064697,0.0349288891324553,0.0891019453741807));
#33335=CARTESIAN_POINT('',(-0.0107387787412939,0.0370721103911615,0.0892342370408473));
#33336=CARTESIAN_POINT('',(-0.012882,0.0383094997618084,0.089366528707514));
#33337=CARTESIAN_POINT('',(-0.0150252212587062,0.0395468891324554,0.0894988203741807));
#33338=CARTESIAN_POINT('',(-0.0175,0.0395468891324554,0.0896311120408473));
#33339=CARTESIAN_POINT('',(-0.0199747787412939,0.0395468891324554,0.0897634037075141));
#33340=CARTESIAN_POINT('',(-0.022118,0.0383094997618084,0.0898956953741807));
#33341=CARTESIAN_POINT('',(-0.0242612212587062,0.0370721103911615,0.0900279870408474));
#33342=CARTESIAN_POINT('',(-0.0254986106293531,0.0349288891324553,0.090160278707514));
#33343=CARTESIAN_POINT('',(-0.0267360000000001,0.0327856678737492,0.0902925703741807));
#33344=CARTESIAN_POINT('',(-0.026736,0.0303108891324553,0.0904248620408474));
#33345=CARTESIAN_POINT('',(-0.026736,0.0303108891324553,0.0904248620408473));
#33346=CARTESIAN_POINT('',(-0.026736,0.0303108891324553,0.0904248620408473));
#33347=CARTESIAN_POINT('',(-0.0267360000000001,0.0278361103911614,0.090557153707514));
#33348=CARTESIAN_POINT('',(-0.0254986106293531,0.0256928891324554,0.0906894453741807));
#33349=CARTESIAN_POINT('',(-0.0242612212587062,0.0235496678737492,0.0908217370408473));
#33350=CARTESIAN_POINT('',(-0.022118,0.0223122785031023,0.090954028707514));
#33351=CARTESIAN_POINT('',(-0.0217493769033143,0.0220994538590013,0.0909767821976795));
#33352=CARTESIAN_POINT('',(-0.0213627414806,0.0219214359766142,0.0909999999999999));
#33353=CARTESIAN_POINT('',(-0.00832342471144782,0.0303108891324553,0.085499093987987));
#33354=CARTESIAN_POINT('',(-0.0175,0.0303108891324553,0.0917));
#33355=CARTESIAN_POINT('',(-0.026736,0.0303108891324553,0.119284271247462));
#33356=CARTESIAN_POINT('',(-0.00832342471144782,0.0303108891324553,0.085499093987987));
#33357=CARTESIAN_POINT('',(-0.026736,0.0303108891324553,0.0935156110802982));
#33358=CARTESIAN_POINT('',(-0.026736,0.0303108891324559,0.093));
#33359=CARTESIAN_POINT('',(-0.026736,0.0303108891324553,0.0935998620408474));
#33360=CARTESIAN_POINT('',(-0.0175,0.0303108891324553,0.093));
#33361=CARTESIAN_POINT('',(-0.0256696111607028,0.0303108891274052,0.092999999842707));
#33362=CARTESIAN_POINT('',(-0.0258790933628727,0.0303108891324553,0.0932356349744546));
#33363=CARTESIAN_POINT('',(-0.0257663813457609,0.0303108891324553,0.0932157608047877));
#33364=CARTESIAN_POINT('',(-0.025676150498743,0.0303108891324553,0.093114263076951));
#33365=CARTESIAN_POINT('',(-0.0256696145170245,0.0303108891324553,0.0929999990740266));
#33366=CARTESIAN_POINT('',(-0.0258790933628727,0.0303108891324553,0.0932356349744546));
#33367=CARTESIAN_POINT('',(-0.0262026,0.0303108891324553,0.0932926779230184));
#33368=CARTESIAN_POINT('',(-0.0265261066371274,0.0303108891324553,0.0933497208715823));
#33369=CARTESIAN_POINT('',(-0.026482,0.0303108891324553,0.0935998620408473));
#33370=CARTESIAN_POINT('',(-0.0208098178710173,0.0387082522117494,0.0927462298951597));
#33371=CARTESIAN_POINT('',(-0.0214329756260445,0.0384626347894019,0.092783915922311));
#33372=CARTESIAN_POINT('',(-0.0220130533185638,0.038127726777475,0.0928205542049156));
#33373=CARTESIAN_POINT('',(-0.024107568652912,0.0369184577853673,0.0929528458715823));
#33374=CARTESIAN_POINT('',(-0.0253168376450197,0.0348239424510191,0.0930851375382489));
#33375=CARTESIAN_POINT('',(-0.0265261066371274,0.0327294271166708,0.0932174292049156));
#33376=CARTESIAN_POINT('',(-0.0265261066371274,0.0303108891324553,0.0933497208715822));
#33377=CARTESIAN_POINT('',(-0.0208563879910611,0.0388264056032331,0.0927686234217097));
#33378=CARTESIAN_POINT('',(-0.0214883137607009,0.0385773322708358,0.092806309448861));
#33379=CARTESIAN_POINT('',(-0.0220765533185638,0.0382377120037556,0.0928429477314656));
#33380=CARTESIAN_POINT('',(-0.0242005391054732,0.0370114282379285,0.0929752393981322));
#33381=CARTESIAN_POINT('',(-0.0254268228713003,0.0348874424510191,0.0931075310647989));
#33382=CARTESIAN_POINT('',(-0.0266531066371274,0.0327634566641096,0.0932398227314656));
#33383=CARTESIAN_POINT('',(-0.0266531066371274,0.0303108891324553,0.0933721143981322));
#33384=CARTESIAN_POINT('',(-0.0208867844781463,0.0389035247524842,0.0928674118847153));
#33385=CARTESIAN_POINT('',(-0.0215244331628801,0.0386521957350017,0.0929050979118666));
#33386=CARTESIAN_POINT('',(-0.022118,0.0383094997618084,0.0929417361944712));
#33387=CARTESIAN_POINT('',(-0.0242612212587062,0.0370721103911615,0.0930740278611379));
#33388=CARTESIAN_POINT('',(-0.0254986106293532,0.0349288891324553,0.0932063195278045));
#33389=CARTESIAN_POINT('',(-0.0267360000000001,0.0327856678737492,0.0933386111944712));
#33390=CARTESIAN_POINT('',(-0.0267360000000001,0.0303108891324553,0.0934709028611378));
#33391=CARTESIAN_POINT('',(-0.0208867844781462,0.0389035247524842,0.0929963710644248));
#33392=CARTESIAN_POINT('',(-0.0215244331628801,0.0386521957350017,0.0930340570915761));
#33393=CARTESIAN_POINT('',(-0.022118,0.0383094997618084,0.0930706953741807));
#33394=CARTESIAN_POINT('',(-0.0242612212587062,0.0370721103911615,0.0932029870408474));
#33395=CARTESIAN_POINT('',(-0.0254986106293531,0.0349288891324553,0.093335278707514));
#33396=CARTESIAN_POINT('',(-0.0267360000000001,0.0327856678737492,0.0934675703741807));
#33397=CARTESIAN_POINT('',(-0.026736,0.0303108891324553,0.0935998620408473));
#33398=CARTESIAN_POINT('',(-0.02444400516351,0.0360772912441661,0.093));
#33399=CARTESIAN_POINT('',(-0.0249336325663123,0.0354876731170587,0.0930432156508374));
#33400=CARTESIAN_POINT('',(-0.0253168376450197,0.0348239424510191,0.0930851375382489));
#33401=CARTESIAN_POINT('',(-0.0265261066371274,0.0327294271166708,0.0932174292049156));
#33402=CARTESIAN_POINT('',(-0.0265261066371274,0.0303108891324553,0.0933497208715822));
#33403=CARTESIAN_POINT('',(-0.0244440051635101,0.0360772912441661,0.093));
#33404=CARTESIAN_POINT('',(-0.0244440051635101,0.0360772912441661,0.093));
#33405=CARTESIAN_POINT('',(-0.0243715488570553,0.0362568694047589,0.093));
#33406=CARTESIAN_POINT('',(-0.0241354058133839,0.0365621839766753,0.0930000000000197));
#33407=CARTESIAN_POINT('',(-0.023645216577888,0.0371396946954097,0.0929999999999886));
#33408=CARTESIAN_POINT('',(-0.0229302657159657,0.037774800623597,0.0930000000000038));
#33409=CARTESIAN_POINT('',(-0.0219837917740965,0.0384065294749524,0.0929999999999989));
#33410=CARTESIAN_POINT('',(-0.0213022700815101,0.0387365742102223,0.093));
#33411=CARTESIAN_POINT('',(-0.0209481246951914,0.0388790938502718,0.093));
#33412=CARTESIAN_POINT('',(-0.0209481246951914,0.0388790938502718,0.093));
#33413=CARTESIAN_POINT('',(-0.0209481246951913,0.0388790938502718,0.093));
#33414=CARTESIAN_POINT('',(-0.0215531734565775,0.0386356025186988,0.0930358311040996));
#33415=CARTESIAN_POINT('',(-0.022118,0.0383094997618084,0.0930706953741807));
#33416=CARTESIAN_POINT('',(-0.0242612212587062,0.0370721103911615,0.0932029870408474));
#33417=CARTESIAN_POINT('',(-0.0254986106293531,0.0349288891324553,0.093335278707514));
#33418=CARTESIAN_POINT('',(-0.0267360000000001,0.0327856678737492,0.0934675703741807));
#33419=CARTESIAN_POINT('',(-0.026736,0.0303108891324553,0.0935998620408473));
#33420=CARTESIAN_POINT('',(-0.0239208501740996,0.0356883202624204,0.0928831027918458));
#33421=CARTESIAN_POINT('',(-0.0245484726165509,0.0349389160261808,0.0929425276418814));
#33422=CARTESIAN_POINT('',(-0.0250350358572561,0.0340954493917498,0.0929985783868971));
#33423=CARTESIAN_POINT('',(-0.0257040731328745,0.0322584121122458,0.093117439776351));
#33424=CARTESIAN_POINT('',(-0.0258752064163071,0.0312736120738746,0.0931781969911814));
#33425=CARTESIAN_POINT('',(-0.0258752064163071,0.0303108891324553,0.0932349496009025));
#33426=CARTESIAN_POINT('',(-0.024087187678253,0.0358276271218958,0.0929213598820724));
#33427=CARTESIAN_POINT('',(-0.0247310692059964,0.0350588089409482,0.092980784732108));
#33428=CARTESIAN_POINT('',(-0.0252302372751709,0.0341934915965639,0.0930368354771236));
#33429=CARTESIAN_POINT('',(-0.0259166065220384,0.0323088643269769,0.0931556968665776));
#33430=CARTESIAN_POINT('',(-0.0260921731565806,0.031298552218392,0.093216454081408));
#33431=CARTESIAN_POINT('',(-0.0260921731565806,0.0303108891324553,0.0932732066911291));
#33432=CARTESIAN_POINT('',(-0.0242535251824065,0.0359669339813711,0.0929596169722989));
#33433=CARTESIAN_POINT('',(-0.0249136657954419,0.0351787018557156,0.0930190418223346));
#33434=CARTESIAN_POINT('',(-0.0254254386930857,0.0342915338013779,0.0930750925673502));
#33435=CARTESIAN_POINT('',(-0.0261291399112023,0.032359316541708,0.0931939539568041));
#33436=CARTESIAN_POINT('',(-0.026309139896854,0.0313234923629095,0.0932547111716345));
#33437=CARTESIAN_POINT('',(-0.026309139896854,0.0303108891324553,0.0933114637813556));
#33438=CARTESIAN_POINT('',(-0.0244198626865599,0.0361062408408464,0.0929978740625255));
#33439=CARTESIAN_POINT('',(-0.0250962623848874,0.0352985947704829,0.0930572989125611));
#33440=CARTESIAN_POINT('',(-0.0256206401110005,0.034389576006192,0.0931133496575767));
#33441=CARTESIAN_POINT('',(-0.0263416733003661,0.032409768756439,0.0932322110470307));
#33442=CARTESIAN_POINT('',(-0.0265261066371274,0.0313484325074269,0.0932929682618611));
#33443=CARTESIAN_POINT('',(-0.0265261066371274,0.0303108891324553,0.0933497208715822));
#33444=CARTESIAN_POINT('',(-0.0174703820743504,0.0303029630442298,0.0931033427178736));
#33445=CARTESIAN_POINT('',(-0.0249879614552658,0.0340711602434389,0.0929999999999981));
#33446=CARTESIAN_POINT('',(-0.0249879614552682,0.0340711602434402,0.093));
#33447=CARTESIAN_POINT('',(-0.0248918662163977,0.0347594676980157,0.093));
#33448=CARTESIAN_POINT('',(-0.0247040214997711,0.0354328579618956,0.093));
#33449=CARTESIAN_POINT('',(-0.0244440051635101,0.0360772912441661,0.093));
#33450=CARTESIAN_POINT('',(-0.0247904637453546,0.0339973612414627,0.0927610698531875));
#33451=CARTESIAN_POINT('',(-0.0256695127292157,0.032258930959684,0.0928803654994113));
#33452=CARTESIAN_POINT('',(-0.0256695127292157,0.0303108891324553,0.0929980941481212));
#33453=CARTESIAN_POINT('',(-0.0247959527978272,0.0340001368178254,0.0928849080708547));
#33454=CARTESIAN_POINT('',(-0.0256756636251824,0.0322603976570276,0.0930042037170785));
#33455=CARTESIAN_POINT('',(-0.0256756636251824,0.0303108891324553,0.0931219323657884));
#33456=CARTESIAN_POINT('',(-0.0248692608122447,0.0340372055091949,0.0929772252855233));
#33457=CARTESIAN_POINT('',(-0.0257578107666889,0.0322799858592798,0.0930965209317472));
#33458=CARTESIAN_POINT('',(-0.0257578107666889,0.0303108891324553,0.093214249580457));
#33459=CARTESIAN_POINT('',(-0.0249774932613182,0.0340919339762356,0.0929986106795209));
#33460=CARTESIAN_POINT('',(-0.0258790933628727,0.0323089060137751,0.0931179063257447));
#33461=CARTESIAN_POINT('',(-0.0258790933628727,0.0303108891324553,0.0932356349744546));
#33462=CARTESIAN_POINT('',(-0.0256696128552748,0.0303108891215471,0.0929999998244189));
#33463=CARTESIAN_POINT('',(-0.0256707191428082,0.0306309045519008,0.0929999998244189));
#33464=CARTESIAN_POINT('',(-0.02563945609545,0.0312704222456812,0.0930000000816386));
#33465=CARTESIAN_POINT('',(-0.0254980011493608,0.0322205044648445,0.0929999999776367));
#33466=CARTESIAN_POINT('',(-0.0253010899158569,0.0329961385140969,0.0930000000027779));
#33467=CARTESIAN_POINT('',(-0.0251208175046229,0.0336100287475924,0.0929999999994444));
#33468=CARTESIAN_POINT('',(-0.025010301394035,0.0339111445489435,0.093));
#33469=CARTESIAN_POINT('',(-0.0249879614552709,0.0340711602434405,0.093));
#33470=CARTESIAN_POINT('',(-0.0175,0.0303108891324553,0.0867173896326779));
#33471=CARTESIAN_POINT('',(-0.0175,0.0303108891324553,0.093));
#33472=CARTESIAN_POINT('',(-0.0175,0.0303108891324553,0.083));
#33473=CARTESIAN_POINT('',(-0.0175,0.0303108891324553,0.083));
#33474=CARTESIAN_POINT('',(-0.0175,0.0303108891324553,0.083));
#33475=CARTESIAN_POINT('',(-0.0055,0.0303108891324553,0.083));
#33476=CARTESIAN_POINT('',(-0.0175,0.0303108891324553,0.093));
#33477=CARTESIAN_POINT('',(-0.0175,0.0303108891324553,0.093));
#33478=CARTESIAN_POINT('',(-0.0055,0.0303108891324553,0.093));
#33479=CARTESIAN_POINT('',(-0.0175,0.0303108891324553,0.091));
#33480=CARTESIAN_POINT('',(-0.0175,0.0303108891324553,0.091));
#33481=CARTESIAN_POINT('',(-0.0175,0.0303108891324553,0.091));
#33482=CARTESIAN_POINT('',(-0.0075,0.0303108891324553,0.091));
#33483=CARTESIAN_POINT('',(-0.0175,0.0303108891324553,0.091));
#33484=CARTESIAN_POINT('',(-0.0175,0.0303108891324553,0.091));
#33485=CARTESIAN_POINT('',(-0.0255,0.0303108891324553,0.091));
#33486=CARTESIAN_POINT('',(-0.0175,0.0303108891324553,0.0917));
#33487=CARTESIAN_POINT('',(-0.0175,0.0303108891324553,0.0917));
#33488=CARTESIAN_POINT('',(-0.0275,0.0303108891324553,0.0917));
#33489=CARTESIAN_POINT('',(-0.0175,0.0303108891324553,0.0917));
#33490=CARTESIAN_POINT('',(-0.0255,0.0303108891324553,0.0917));
#33491=CARTESIAN_POINT('',(-0.0175,0.0303108891324553,0.083));
#33492=CARTESIAN_POINT('',(-0.0175,0.0303108891324553,0.0917));
#33493=CARTESIAN_POINT('',(-0.0175,0.0303108891324553,0.119284271247462));
#33494=CARTESIAN_POINT('',(-0.0175,0.0303108891324553,0.093));
#45463=MECHANICAL_DESIGN_GEOMETRIC_PRESENTATION_REPRESENTATION('',(#13538),#45464);
#45464=(
GEOMETRIC_REPRESENTATION_CONTEXT(3)
GLOBAL_UNCERTAINTY_ASSIGNED_CONTEXT((#45492))
GLOBAL_UNIT_ASSIGNED_CONTEXT((#45522,#45521,#45520))
REPRESENTATION_CONTEXT('MAS-690','TOP_LEVEL_ASSEMBLY_PART')
);
#45474=(
GEOMETRIC_REPRESENTATION_CONTEXT(3)
GLOBAL_UNCERTAINTY_ASSIGNED_CONTEXT((#45502))
GLOBAL_UNIT_ASSIGNED_CONTEXT((#45522,#45521,#45520))
REPRESENTATION_CONTEXT('refill_cap','COMPONENT_PART')
);
#45492=UNCERTAINTY_MEASURE_WITH_UNIT(LENGTH_MEASURE(1.E-8),#45522,
'DISTANCE_ACCURACY_VALUE','Maximum Tolerance applied to model');
#45502=UNCERTAINTY_MEASURE_WITH_UNIT(LENGTH_MEASURE(2.E-5),#45522,
'DISTANCE_ACCURACY_VALUE','Maximum Tolerance applied to model');
#45520=(
NAMED_UNIT(*)
SI_UNIT($,.STERADIAN.)
SOLID_ANGLE_UNIT()
);
#45521=(
NAMED_UNIT(*)
PLANE_ANGLE_UNIT()
SI_UNIT($,.RADIAN.)
);
#45522=(
LENGTH_UNIT()
NAMED_UNIT(*)
SI_UNIT($,.METRE.)
);
#45544=PRODUCT_DEFINITION_SHAPE('','',#45595);
#45595=PRODUCT_DEFINITION('','',#45651,#45623);
#45623=PRODUCT_DEFINITION_CONTEXT('',#45782,'design');
#45651=PRODUCT_DEFINITION_FORMATION_WITH_SPECIFIED_SOURCE('','',#45707,
 .NOT_KNOWN.);
#45707=PRODUCT('refill_cap','refill_cap','refill_cap',(#45763));
#45763=PRODUCT_CONTEXT('',#45782,'mechanical');
#45782=APPLICATION_CONTEXT('managed model based 3d engineering');
ENDSEC;
END-ISO-10303-21;
